ISO-10303-21;
HEADER;
FILE_DESCRIPTION (('STEP AP214'),
    '1' );
FILE_NAME ('Flange.step',
    '2026-10-09T10:51:02',
    ( '' ),
    ( '' ),
    'SwSTEP 2.0',
    'SolidWorks 2026',
    '' );
FILE_SCHEMA (( 'AUTOMOTIVE_DESIGN' ));
ENDSEC;

DATA;
#2=EDGE_CURVE ( 'NONE', #15659, #11181, #7452, .T. ) ;
#33=AXIS2_PLACEMENT_3D ( 'NONE', #9862, #17006, #490 ) ;
#35=ORIENTED_EDGE ( 'NONE', *, *, #1256, .T. ) ;
#40=UNCERTAINTY_MEASURE_WITH_UNIT (LENGTH_MEASURE( 1.000000000000000082E-05 ), #13566, 'distance_accuracy_value', 'NONE');
#47=DIRECTION ( 'NONE',  ( 0.01292394549866738782, 0.005513023399720468239, 0.9999012842304692006 ) ) ;
#48=CARTESIAN_POINT ( 'NONE',  ( -5.718390838975437873, 144.0378302125689629, 276.6767821598265300 ) ) ;
#68=EDGE_LOOP ( 'NONE', ( #15099, #11264, #5620 ) ) ;
#72=EDGE_CURVE ( 'NONE', #164, #20449, #17392, .T. ) ;
#76=CARTESIAN_POINT ( 'NONE',  ( 51.43549903698339421, 154.9275132768233618, 276.0443355225219761 ) ) ;
#90=ORIENTED_EDGE ( 'NONE', *, *, #19194, .F. ) ;
#95=CIRCLE ( 'NONE', #9269, 21.67179167071592261 ) ;
#130=AXIS2_PLACEMENT_3D ( 'NONE', #8032, #9876, #20201 ) ;
#144=EDGE_LOOP ( 'NONE', ( #22040, #16025, #1524, #21274, #7268, #9424, #8449, #10368, #9326, #4340 ) ) ;
#145=CARTESIAN_POINT ( 'NONE',  ( 20.36241020427591053, 184.0347753543214537, 278.2158687833080535 ) ) ;
#158=VECTOR ( 'NONE', #9778, 1000.000000000000000 ) ;
#164=VERTEX_POINT ( 'NONE', #8472 ) ;
#201=LINE ( 'NONE', #14344, #11898 ) ;
#256=CARTESIAN_POINT ( 'NONE',  ( 48.39260390757410590, 174.4164586986524057, 267.9754221921975272 ) ) ;
#266=ORIENTED_EDGE ( 'NONE', *, *, #3629, .T. ) ;
#267=ADVANCED_FACE ( 'NONE', ( #15553 ), #14170, .F. ) ;
#317=TOROIDAL_SURFACE ( 'NONE', #19007, 12.37020706055087516, 2.000000000000000000 ) ;
#339=ORIENTED_EDGE ( 'NONE', *, *, #11190, .F. ) ;
#345=VERTEX_POINT ( 'NONE', #76 ) ;
#363=AXIS2_PLACEMENT_3D ( 'NONE', #1584, #20516, #11935 ) ;
#388=EDGE_CURVE ( 'NONE', #8063, #7165, #5071, .T. ) ;
#389=AXIS2_PLACEMENT_3D ( 'NONE', #2582, #21844, #9353 ) ;
#401=CIRCLE ( 'NONE', #33, 1.999999999999997780 ) ;
#406=EDGE_CURVE ( 'NONE', #20552, #2150, #13382, .T. ) ;
#414=CIRCLE ( 'NONE', #19108, 7.500000000000002665 ) ;
#425=ORIENTED_EDGE ( 'NONE', *, *, #15905, .T. ) ;
#447=EDGE_LOOP ( 'NONE', ( #11698, #17092 ) ) ;
#485=ORIENTED_EDGE ( 'NONE', *, *, #21713, .T. ) ;
#489=FACE_BOUND ( 'NONE', #18864, .T. ) ;
#490=DIRECTION ( 'NONE',  ( -0.6916826046072642731, -0.7220860138273257345, 0.01292142092318428193 ) ) ;
#517=CARTESIAN_POINT ( 'NONE',  ( 15.33595178936205627, 187.7751029041553466, 277.1220671345521964 ) ) ;
#584=EDGE_CURVE ( 'NONE', #17705, #14146, #2869, .T. ) ;
#598=DIRECTION ( 'NONE',  ( 0.009760756503428015193, -0.9999378516499566327, 0.005387065077612487526 ) ) ;
#599=DIRECTION ( 'NONE',  ( -0.9726991065672923042, -0.2316562896908775926, 0.01384960395994898341 ) ) ;
#609=LINE ( 'NONE', #11282, #2017 ) ;
#641=EDGE_CURVE ( 'NONE', #9573, #8236, #22254, .T. ) ;
#678=FACE_OUTER_BOUND ( 'NONE', #20422, .T. ) ;
#691=CYLINDRICAL_SURFACE ( 'NONE', #4585, 7.500000000000002665 ) ;
#700=ORIENTED_EDGE ( 'NONE', *, *, #10816, .F. ) ;
#704=DIRECTION ( 'NONE',  ( -0.01292394549866738782, -0.005513023399720468239, -0.9999012842304692006 ) ) ;
#707=FACE_OUTER_BOUND ( 'NONE', #16939, .T. ) ;
#718=DIRECTION ( 'NONE',  ( 0.01292394549866738782, 0.005513023399720468239, 0.9999012842304692006 ) ) ;
#727=ORIENTED_EDGE ( 'NONE', *, *, #19452, .T. ) ;
#748=DIRECTION ( 'NONE',  ( 0.7084451806051504930, 0.7056452299526748684, -0.01304743355500855191 ) ) ;
#752=APPLICATION_CONTEXT ( 'automotive_design' ) ;
#790=CIRCLE ( 'NONE', #8837, 7.500000000000002665 ) ;
#808=DIRECTION ( 'NONE',  ( 0.01292394549866738782, 0.005513023399720468239, 0.9999012842304692006 ) ) ;
#830=FACE_OUTER_BOUND ( 'NONE', #13990, .T. ) ;
#849=EDGE_LOOP ( 'NONE', ( #339, #9089, #22049 ) ) ;
#872=VECTOR ( 'NONE', #6599, 1000.000000000000114 ) ;
#890=CARTESIAN_POINT ( 'NONE',  ( 9.882012489055451709, 190.0684914133515235, 274.6858930762247724 ) ) ;
#895=B_SPLINE_CURVE_WITH_KNOTS ( 'NONE', 3,
 ( #10817, #13911, #20904, #5159, #12201, #19184, #3561, #2076, #9055, #1735 ),
 .UNSPECIFIED., .F., .F.,
 ( 4, 2, 2, 2, 4 ),
 ( -3.258122103462694725E-05, 0.003484391791828337151, 0.007001364804691301812, 0.01051833781755426647, 0.01403531083041723027 ),
 .UNSPECIFIED. ) ;
#963=EDGE_CURVE ( 'NONE', #17869, #1319, #1138, .T. ) ;
#976=PLANE ( 'NONE',  #10321 ) ;
#994=CARTESIAN_POINT ( 'NONE',  ( 8.732865712828660421, 190.3249964942741883, 274.4707185275763095 ) ) ;
#996=LINE ( 'NONE', #11330, #11879 ) ;
#1012=VECTOR ( 'NONE', #8429, 999.9999999999998863 ) ;
#1013=CARTESIAN_POINT ( 'NONE',  ( 20.72345578460594595, 149.3062324992208687, 276.4722887938682447 ) ) ;
#1023=FACE_BOUND ( 'NONE', #13475, .T. ) ;
#1028=FACE_OUTER_BOUND ( 'NONE', #3545, .T. ) ;
#1060=CARTESIAN_POINT ( 'NONE',  ( -44.86761910970069778, 151.3223208568695952, 257.3069776102678929 ) ) ;
#1093=CARTESIAN_POINT ( 'NONE',  ( -10.86881930386964790, 187.2152970740215494, 276.3440875669132879 ) ) ;
#1112=DIRECTION ( 'NONE',  ( 0.009760756503427994377, -0.9999378516499565217, 0.005387065077612505741 ) ) ;
#1118=AXIS2_PLACEMENT_3D ( 'NONE', #18244, #2275, #16321 ) ;
#1128=CIRCLE ( 'NONE', #3294, 2.000000000000005329 ) ;
#1134=FACE_OUTER_BOUND ( 'NONE', #5167, .T. ) ;
#1138=LINE ( 'NONE', #13326, #1012 ) ;
#1147=AXIS2_PLACEMENT_3D ( 'NONE', #3483, #14186, #8983 ) ;
#1174=CIRCLE ( 'NONE', #13648, 1.999999999999998890 ) ;
#1194=ORIENTED_EDGE ( 'NONE', *, *, #21713, .F. ) ;
#1211=CARTESIAN_POINT ( 'NONE',  ( -11.21898953668323173, 147.2569162822765350, 277.2143219418639433 ) ) ;
#1219=CARTESIAN_POINT ( 'NONE',  ( -12.01599076143180511, 185.1584625638569435, 277.0076056079356590 ) ) ;
#1226=EDGE_CURVE ( 'NONE', #18377, #16716, #5180, .T. ) ;
#1256=EDGE_CURVE ( 'NONE', #9573, #164, #19683, .T. ) ;
#1260=CARTESIAN_POINT ( 'NONE',  ( 9.196690372329099361, 142.8086146031528187, 274.7267082784171066 ) ) ;
#1261=LINE ( 'NONE', #15499, #12091 ) ;
#1273=CARTESIAN_POINT ( 'NONE',  ( -44.77337549856770238, 180.0561670719389724, 275.2189164286555751 ) ) ;
#1316=DIRECTION ( 'NONE',  ( -0.01257542709085761497, -0.04040699277118586091, -0.9991041655246323261 ) ) ;
#1319=VERTEX_POINT ( 'NONE', #12900 ) ;
#1324=CARTESIAN_POINT ( 'NONE',  ( -8.866921938745853993, 144.9029155259317179, 276.3123546325696225 ) ) ;
#1330=CARTESIAN_POINT ( 'NONE',  ( -10.69950344851409163, 186.1885126486754700, 276.9478893194735747 ) ) ;
#1331=VERTEX_POINT ( 'NONE', #16367 ) ;
#1340=CARTESIAN_POINT ( 'NONE',  ( 20.72467744229798825, 186.0120790718647754, 276.2495570520306387 ) ) ;
#1362=CARTESIAN_POINT ( 'NONE',  ( 18.01056092802276964, 145.8310346079609872, 276.1989901147027240 ) ) ;
#1395=DIRECTION ( 'NONE',  ( 1.000000000000000000, 0.000000000000000000, 0.000000000000000000 ) ) ;
#1422=ORIENTED_EDGE ( 'NONE', *, *, #641, .T. ) ;
#1428=DIRECTION ( 'NONE',  ( 0.01292394549866738782, 0.005513023399720468239, 0.9999012842304692006 ) ) ;
#1430=CARTESIAN_POINT ( 'NONE',  ( -2.684107246038483385, 142.9527971194642078, 275.3366952467220017 ) ) ;
#1447=CARTESIAN_POINT ( 'NONE',  ( 3.833582208905060185, 166.6352317792379267, 296.5970240496429255 ) ) ;
#1448=CARTESIAN_POINT ( 'NONE',  ( 19.50571343488122267, 184.8272563654908538, 278.1819008152489232 ) ) ;
#1458=CARTESIAN_POINT ( 'NONE',  ( 48.56920114533915722, 166.9610289984755127, 276.0150354541233924 ) ) ;
#1468=CARTESIAN_POINT ( 'NONE',  ( 48.56920114533915722, 166.9610289984755127, 276.0150354541233924 ) ) ;
#1514=CARTESIAN_POINT ( 'NONE',  ( -14.93612093091044102, 185.1121758471145142, 276.7357782268812798 ) ) ;
#1524=ORIENTED_EDGE ( 'NONE', *, *, #4986, .T. ) ;
#1535=CARTESIAN_POINT ( 'NONE',  ( 10.04616666026851313, 189.9867745584397767, 275.0214033402720588 ) ) ;
#1539=CARTESIAN_POINT ( 'NONE',  ( -12.04904146786470776, 146.2738556374876282, 276.7751546531125655 ) ) ;
#1541=VECTOR ( 'NONE', #19976, 999.9999999999998863 ) ;
#1549=ORIENTED_EDGE ( 'NONE', *, *, #6294, .F. ) ;
#1567=DIRECTION ( 'NONE',  ( 0.01292394549866738782, 0.005513023399720468239, 0.9999012842304692006 ) ) ;
#1584=CARTESIAN_POINT ( 'NONE',  ( 48.56920114533915722, 166.9610289984755127, 276.0150354541233924 ) ) ;
#1598=DIRECTION ( 'NONE',  ( 0.01292394549866738782, 0.005513023399720468239, 0.9999012842304692006 ) ) ;
#1628=VECTOR ( 'NONE', #7640, 999.9999999999998863 ) ;
#1643=CARTESIAN_POINT ( 'NONE',  ( -44.86761910970069778, 151.3223208568695952, 257.3069776102678929 ) ) ;
#1644=ORIENTED_EDGE ( 'NONE', *, *, #7964, .T. ) ;
#1647=CARTESIAN_POINT ( 'NONE',  ( -11.78710887361312132, 185.2757727756024622, 278.4447062962351538 ) ) ;
#1673=CARTESIAN_POINT ( 'NONE',  ( 51.43549903698337999, 154.9275132768233618, 276.0443355225219761 ) ) ;
#1684=CARTESIAN_POINT ( 'NONE',  ( 3.316624388958365088, 166.4147108432491109, 256.6009726804241495 ) ) ;
#1689=B_SPLINE_CURVE_WITH_KNOTS ( 'NONE', 3,
 ( #12813, #20028, #11315, #11410, #21726, #18300, #21937, #13260, #7736, #9448, #4165, #2568 ),
 .UNSPECIFIED., .F., .F.,
 ( 4, 2, 2, 2, 2, 4 ),
 ( 0.000000000000000000, 0.003508523874122987905, 0.007017047748245975811, 0.01052557162236896285, 0.01227983355943044162, 0.01403409549649192040 ),
 .UNSPECIFIED. ) ;
#1694=CARTESIAN_POINT ( 'NONE',  ( 16.39796002119450335, 145.1381702172243706, 275.9805542436448036 ) ) ;
#1699=CARTESIAN_POINT ( 'NONE',  ( 51.17420407245305825, 179.0367939709223606, 273.9145872160426620 ) ) ;
#1725=VERTEX_POINT ( 'NONE', #5958 ) ;
#1735=CARTESIAN_POINT ( 'NONE',  ( 21.71998689217155132, 185.4674263880815204, 276.2600312189053966 ) ) ;
#1741=ORIENTED_EDGE ( 'NONE', *, *, #16059, .F. ) ;
#1771=CARTESIAN_POINT ( 'NONE',  ( -3.701274867523290713, 143.2855812733562288, 275.7914880546696281 ) ) ;
#1787=EDGE_LOOP ( 'NONE', ( #18482, #19485 ) ) ;
#1827=CARTESIAN_POINT ( 'NONE',  ( 3.600951189929047391, 166.5359973580429482, 278.5988009334944877 ) ) ;
#1887=CARTESIAN_POINT ( 'NONE',  ( -8.165269366632555759, 145.2835741796170623, 277.6601055409479386 ) ) ;
#1891=B_SPLINE_CURVE_WITH_KNOTS ( 'NONE', 3,
 ( #22507, #7458, #2064, #14497, #21457, #8519, #6800, #13824, #9045, #17390, #20808, #19086, #1647, #3360, #10377, #5178 ),
 .UNSPECIFIED., .F., .F.,
 ( 4, 2, 2, 2, 2, 2, 2, 4 ),
 ( -3.123367963899254272E-05, 0.001725203944011495299, 0.003481641567661983121, 0.006994516814962895880, 0.008750954438613373076, 0.01050739206226384941, 0.01226382968591432573, 0.01402026730956480380 ),
 .UNSPECIFIED. ) ;
#1949=DIRECTION ( 'NONE',  ( 0.009760756503427813965, -0.9999378516499565217, 0.005387065077607405654 ) ) ;
#1983=DIRECTION ( 'NONE',  ( 0.01292394549866738955, 0.005513023399720468239, 0.9999012842304693116 ) ) ;
#2017=VECTOR ( 'NONE', #16254, 1000.000000000000114 ) ;
#2027=ORIENTED_EDGE ( 'NONE', *, *, #6679, .F. ) ;
#2064=CARTESIAN_POINT ( 'NONE',  ( -3.133037003347189042, 189.9394842237717569, 275.0803702628431893 ) ) ;
#2072=CARTESIAN_POINT ( 'NONE',  ( 14.28162271022098295, 144.6901722051186994, 276.8194863368150891 ) ) ;
#2076=CARTESIAN_POINT ( 'NONE',  ( 19.65277869176573233, 186.5675413641987461, 276.1968354304440254 ) ) ;
#2109=CARTESIAN_POINT ( 'NONE',  ( -44.31114033011734676, 178.1114032988642748, 275.1538586390841488 ) ) ;
#2150=VERTEX_POINT ( 'NONE', #15925 ) ;
#2206=ORIENTED_EDGE ( 'NONE', *, *, #3114, .F. ) ;
#2216=EDGE_CURVE ( 'NONE', #16406, #14784, #2886, .T. ) ;
#2220=CARTESIAN_POINT ( 'NONE',  ( -4.209144317661589696, 143.4607783881357932, 276.0169400659812595 ) ) ;
#2241=AXIS2_PLACEMENT_3D ( 'NONE', #1458, #1567, #9957 ) ;
#2242=CARTESIAN_POINT ( 'NONE',  ( 51.78636885665599721, 152.2590373701827957, 256.0525387646090394 ) ) ;
#2254=ORIENTED_EDGE ( 'NONE', *, *, #19029, .F. ) ;
#2264=CARTESIAN_POINT ( 'NONE',  ( 3.808636396294353688, 166.6245905359224082, 294.6670135843256162 ) ) ;
#2275=DIRECTION ( 'NONE',  ( 0.01292394549866738782, 0.005513023399720468239, 0.9999012842304692006 ) ) ;
#2324=DIRECTION ( 'NONE',  ( 0.01292394549866738782, 0.005513023399720468239, 0.9999012842304692006 ) ) ;
#2329=CIRCLE ( 'NONE', #4881, 7.500000000000002665 ) ;
#2335=AXIS2_PLACEMENT_3D ( 'NONE', #21523, #7763, #16405 ) ;
#2338=EDGE_CURVE ( 'NONE', #4798, #2150, #15746, .T. ) ;
#2347=CARTESIAN_POINT ( 'NONE',  ( 10.82486875048587827, 189.7530090480866534, 275.3475331242451034 ) ) ;
#2366=DIRECTION ( 'NONE',  ( 0.01292394549866738782, 0.005513023399720468239, 0.9999012842304692006 ) ) ;
#2374=MANIFOLD_SOLID_BREP ( 'Stock-MAS-425-1', #12086 ) ;
#2383=CARTESIAN_POINT ( 'NONE',  ( 8.332717885210684017, 188.3826505299215057, 276.4169913494580442 ) ) ;
#2398=CIRCLE ( 'NONE', #8245, 4.200000000000005507 ) ;
#2419=ORIENTED_EDGE ( 'NONE', *, *, #963, .F. ) ;
#2439=CARTESIAN_POINT ( 'NONE',  ( 48.56920114533915722, 166.9610289984755127, 276.0150354541233924 ) ) ;
#2443=CARTESIAN_POINT ( 'NONE',  ( -44.86761910970069778, 151.3223208568695952, 257.3069776102678929 ) ) ;
#2446=LINE ( 'NONE', #20225, #14996 ) ;
#2495=CARTESIAN_POINT ( 'NONE',  ( 22.11217541977124057, 147.9487928221719812, 278.4620210716466886 ) ) ;
#2497=ORIENTED_EDGE ( 'NONE', *, *, #10853, .T. ) ;
#2518=ORIENTED_EDGE ( 'NONE', *, *, #19667, .T. ) ;
#2521=DIRECTION ( 'NONE',  ( 0.009760756503427813965, -0.9999378516499565217, 0.005387065077607405654 ) ) ;
#2568=CARTESIAN_POINT ( 'NONE',  ( -2.096375399687102625, 190.2200455327031818, 274.6112675210154634 ) ) ;
#2569=CARTESIAN_POINT ( 'NONE',  ( 20.36241020427591408, 184.0347753543214537, 278.2158687833079966 ) ) ;
#2582=CARTESIAN_POINT ( 'NONE',  ( 48.56920114533915722, 166.9610289984755127, 276.0150354541233924 ) ) ;
#2584=ORIENTED_EDGE ( 'NONE', *, *, #5219, .T. ) ;
#2623=EDGE_CURVE ( 'NONE', #1319, #3811, #6197, .T. ) ;
#2627=VERTEX_POINT ( 'NONE', #21239 ) ;
#2642=CARTESIAN_POINT ( 'NONE',  ( -2.000285031460978580, 141.9874903446699363, 256.8043760453134610 ) ) ;
#2668=CARTESIAN_POINT ( 'NONE',  ( -6.065819164189576007, 143.9013245968714045, 275.7904085731360055 ) ) ;
#2672=ADVANCED_FACE ( 'NONE', ( #1028 ), #13202, .T. ) ;
#2678=AXIS2_PLACEMENT_3D ( 'NONE', #18936, #20663, #5141 ) ;
#2681=DIRECTION ( 'NONE',  ( -0.009760756503428009989, 0.9999378516499564107, -0.005387065077611111891 ) ) ;
#2702=DIRECTION ( 'NONE',  ( 0.01292394549866738782, 0.005513023399720468239, 0.9999012842304692006 ) ) ;
#2720=DIRECTION ( 'NONE',  ( 0.9770372205688161449, -0.2127605332646572978, -0.01145535281434410108 ) ) ;
#2727=LINE ( 'NONE', #6164, #9216 ) ;
#2737=AXIS2_PLACEMENT_3D ( 'NONE', #3326, #10348, #10568 ) ;
#2789=AXIS2_PLACEMENT_3D ( 'NONE', #17496, #20802, #6796 ) ;
#2790=FILL_AREA_STYLE_COLOUR ( '', #9106 ) ;
#2796=DIRECTION ( 'NONE',  ( 0.01292394549866738782, 0.005513023399720468239, 0.9999012842304692006 ) ) ;
#2821=CARTESIAN_POINT ( 'NONE',  ( 19.19569574945376544, 186.7745716580498367, 276.1480060676194057 ) ) ;
#2825=DIRECTION ( 'NONE',  ( 0.009760756503428009989, -0.9999378516499564107, 0.005387065077611111891 ) ) ;
#2842=CARTESIAN_POINT ( 'NONE',  ( 20.70083805927511733, 149.3646325075532957, 278.4026507072620120 ) ) ;
#2849=CARTESIAN_POINT ( 'NONE',  ( -2.096375399687102625, 190.2200455327031818, 274.6112675210154634 ) ) ;
#2854=CARTESIAN_POINT ( 'NONE',  ( 14.71507153966036974, 144.4759177913303745, 275.7214514730162591 ) ) ;
#2869=LINE ( 'NONE', #11958, #17891 ) ;
#2881=ADVANCED_FACE ( 'NONE', ( #20762 ), #17342, .T. ) ;
#2882=ORIENTED_EDGE ( 'NONE', *, *, #18755, .F. ) ;
#2884=EDGE_CURVE ( 'NONE', #17869, #6385, #19760, .T. ) ;
#2886=CIRCLE ( 'NONE', #5446, 7.500000000000002665 ) ;
#2890=ORIENTED_EDGE ( 'NONE', *, *, #19666, .F. ) ;
#2903=AXIS2_PLACEMENT_3D ( 'NONE', #8686, #5017, #3185 ) ;
#2909=CARTESIAN_POINT ( 'NONE',  ( -12.47967489686980613, 148.2895124671312317, 277.1262451100013777 ) ) ;
#2926=EDGE_CURVE ( 'NONE', #6314, #17705, #18678, .T. ) ;
#2927=CARTESIAN_POINT ( 'NONE',  ( 17.62344600982285314, 187.4828202841882216, 275.9769641099970841 ) ) ;
#2936=ORIENTED_EDGE ( 'NONE', *, *, #19029, .T. ) ;
#2948=CARTESIAN_POINT ( 'NONE',  ( 20.37582863626993301, 148.9655229296736820, 276.6108942144915659 ) ) ;
#2953=ORIENTED_EDGE ( 'NONE', *, *, #19666, .T. ) ;
#2954=CARTESIAN_POINT ( 'NONE',  ( 51.20005196345039167, 179.0478200177218184, 275.9143897845036122 ) ) ;
#2974=PRODUCT_CONTEXT ( 'NONE', #20689, 'mechanical' ) ;
#2978=ORIENTED_EDGE ( 'NONE', *, *, #20157, .F. ) ;
#3000=( NAMED_UNIT ( * ) PLANE_ANGLE_UNIT ( ) SI_UNIT ( $, .RADIAN. ) );
#3015=DIRECTION ( 'NONE',  ( 0.009760756503428048153, -0.9999378516499565217, 0.005387065077612505741 ) ) ;
#3022=FACE_OUTER_BOUND ( 'NONE', #68, .T. ) ;
#3031=CARTESIAN_POINT ( 'NONE',  ( -7.355408695361009386, 188.2724542843479867, 276.2720482804903099 ) ) ;
#3044=CARTESIAN_POINT ( 'NONE',  ( 15.34924354053137741, 187.7676347092321407, 277.1267350366562709 ) ) ;
#3058=DIRECTION ( 'NONE',  ( 0.01292394549866738955, 0.005513023399720468239, 0.9999012842304693116 ) ) ;
#3094=DIRECTION ( 'NONE',  ( -0.01292394549866738782, -0.005513023399720468239, -0.9999012842304692006 ) ) ;
#3102=CARTESIAN_POINT ( 'NONE',  ( 0.000000000000000000, 0.000000000000000000, 0.000000000000000000 ) ) ;
#3114=EDGE_CURVE ( 'NONE', #9573, #4798, #14502, .T. ) ;
#3131=CARTESIAN_POINT ( 'NONE',  ( -44.04984536558698238, 154.0021226047651908, 277.2836069455634060 ) ) ;
#3140=ORIENTED_EDGE ( 'NONE', *, *, #20593, .T. ) ;
#3169=CARTESIAN_POINT ( 'NONE',  ( 18.74581175270508027, 147.5432771199994875, 276.8255568971947582 ) ) ;
#3177=CARTESIAN_POINT ( 'NONE',  ( 21.74583478316889185, 185.4784524348809782, 278.2598337873663468 ) ) ;
#3185=DIRECTION ( 'NONE',  ( -0.2317097747526812579, 0.9727820773532223075, -0.002368599673008277024 ) ) ;
#3201=( NAMED_UNIT ( * ) PLANE_ANGLE_UNIT ( ) SI_UNIT ( $, .RADIAN. ) );
#3232=DIRECTION ( 'NONE',  ( 0.009760756503427813965, -0.9999378516499565217, 0.005387065077607405654 ) ) ;
#3235=CARTESIAN_POINT ( 'NONE',  ( -8.910000229846922082, 145.6729472732380088, 276.9535057578845567 ) ) ;
#3240=CARTESIAN_POINT ( 'NONE',  ( 3.808636396294353688, 166.6245905359224082, 294.6670135843256162 ) ) ;
#3263=AXIS2_PLACEMENT_3D ( 'NONE', #14223, #7422, #21199 ) ;
#3277=CARTESIAN_POINT ( 'NONE',  ( 10.25516029832731846, 143.0782243734045949, 275.1688085660350680 ) ) ;
#3294=AXIS2_PLACEMENT_3D ( 'NONE', #16390, #748, #21507 ) ;
#3308=EDGE_LOOP ( 'NONE', ( #6133, #6546, #7347, #21466 ) ) ;
#3314=AXIS2_PLACEMENT_3D ( 'NONE', #4143, #718, #7713 ) ;
#3326=CARTESIAN_POINT ( 'NONE',  ( -41.41899454747574083, 166.0889136240115249, 277.1829612759436827 ) ) ;
#3334=LINE ( 'NONE', #22594, #15400 ) ;
#3360=CARTESIAN_POINT ( 'NONE',  ( -12.65647975835393169, 184.5194971381093580, 278.5989247057070770 ) ) ;
#3371=ORIENTED_EDGE ( 'NONE', *, *, #2623, .T. ) ;
#3393=AXIS2_PLACEMENT_3D ( 'NONE', #7168, #47, #11036 ) ;
#3406=CARTESIAN_POINT ( 'NONE',  ( 3.316624388958365088, 166.4147108432491109, 256.6009726804241495 ) ) ;
#3407=CARTESIAN_POINT ( 'NONE',  ( 15.74005880004537872, 145.5104308052777640, 277.3467734109414664 ) ) ;
#3416=DIRECTION ( 'NONE',  ( 0.009760756503427813965, -0.9999378516499565217, 0.005387065077607405654 ) ) ;
#3437=DIRECTION ( 'NONE',  ( 0.009760756503428003050, -0.9999378516499565217, 0.005387065077610373766 ) ) ;
#3448=DIRECTION ( 'NONE',  ( 0.009760756503427210282, -0.9999378516499566327, 0.005387065077606872227 ) ) ;
#3469=CARTESIAN_POINT ( 'NONE',  ( -41.41899454747574083, 166.0889136240115249, 277.1829612759436827 ) ) ;
#3483=CARTESIAN_POINT ( 'NONE',  ( 3.575103298931712636, 166.5249713112435188, 276.5989983650335375 ) ) ;
#3518=ORIENTED_EDGE ( 'NONE', *, *, #6996, .F. ) ;
#3521=CARTESIAN_POINT ( 'NONE',  ( -14.93612093091044102, 185.1121758471145142, 276.7357782268812798 ) ) ;
#3522=DIRECTION ( 'NONE',  ( 0.01292394549866738955, 0.005513023399720468239, 0.9999012842304693116 ) ) ;
#3535=FACE_OUTER_BOUND ( 'NONE', #15370, .T. ) ;
#3545=EDGE_LOOP ( 'NONE', ( #21188, #6956, #16754, #21492 ) ) ;
#3549=ADVANCED_FACE ( 'NONE', ( #12736 ), #4317, .F. ) ;
#3561=CARTESIAN_POINT ( 'NONE',  ( 17.53646115355174828, 187.5322632972278711, 275.9756305834653176 ) ) ;
#3575=CARTESIAN_POINT ( 'NONE',  ( 20.38408663817444477, 184.0728056720850532, 276.2849873611855855 ) ) ;
#3622=FACE_BOUND ( 'NONE', #10317, .T. ) ;
#3629=EDGE_CURVE ( 'NONE', #12879, #6995, #2446, .T. ) ;
#3636=ORIENTED_EDGE ( 'NONE', *, *, #20441, .F. ) ;
#3685=CONICAL_SURFACE ( 'NONE', #8448, 24.99999999999998224, 0.03490658503988662564 ) ;
#3691=ORIENTED_EDGE ( 'NONE', *, *, #1226, .F. ) ;
#3712=CARTESIAN_POINT ( 'NONE',  ( -12.73484320226976863, 148.6269210710419486, 278.8388817128882238 ) ) ;
#3745=DIRECTION ( 'NONE',  ( 0.009760756503427210282, -0.9999378516499566327, 0.005387065077606872227 ) ) ;
#3749=ORIENTED_EDGE ( 'NONE', *, *, #8631, .T. ) ;
#3807=DIRECTION ( 'NONE',  ( -0.2126763768167737323, -0.9770888199431678744, 0.008136134595576589509 ) ) ;
#3811=VERTEX_POINT ( 'NONE', #17246 ) ;
#3845=DIRECTION ( 'NONE',  ( 0.9998688410312766006, 0.009690170827377627902, -0.01297695357578096571 ) ) ;
#3856=ADVANCED_FACE ( 'NONE', ( #15428 ), #18372, .F. ) ;
#3885=CYLINDRICAL_SURFACE ( 'NONE', #15169, 7.999999999999985789 ) ;
#3896=CARTESIAN_POINT ( 'NONE',  ( 19.85551708207331245, 148.5512754185721462, 278.3770131723069312 ) ) ;
#3910=DIRECTION ( 'NONE',  ( 0.2317097747526812579, -0.9727820773532223075, 0.002368599673008277024 ) ) ;
#3934=DIRECTION ( 'NONE',  ( 0.01292394549866738608, 0.005513023399720468239, 0.9999012842304692006 ) ) ;
#3939=CARTESIAN_POINT ( 'NONE',  ( 20.36241020427591408, 184.0347753543214537, 278.2158687833079966 ) ) ;
#3965=ORIENTED_EDGE ( 'NONE', *, *, #10786, .F. ) ;
#3972=ORIENTED_EDGE ( 'NONE', *, *, #21272, .F. ) ;
#4025=CARTESIAN_POINT ( 'NONE',  ( 3.575103298931712636, 166.5249713112435188, 276.5989983650335375 ) ) ;
#4030=AXIS2_PLACEMENT_3D ( 'NONE', #7902, #20062, #14938 ) ;
#4048=CARTESIAN_POINT ( 'NONE',  ( -10.05852611029434307, 146.4821163384300462, 278.3017991042662516 ) ) ;
#4131=AXIS2_PLACEMENT_3D ( 'NONE', #8906, #19473, #3745 ) ;
#4143=CARTESIAN_POINT ( 'NONE',  ( -41.41899454747574083, 166.0889136240115249, 277.1829612759436827 ) ) ;
#4165=CARTESIAN_POINT ( 'NONE',  ( -2.652335923087511205, 190.0839019912061758, 274.7308922624509933 ) ) ;
#4177=EDGE_CURVE ( 'NONE', #20449, #18377, #1689, .T. ) ;
#4210=ORIENTED_EDGE ( 'NONE', *, *, #20593, .F. ) ;
#4216=ADVANCED_FACE ( 'NONE', ( #11296 ), #317, .T. ) ;
#4256=CARTESIAN_POINT ( 'NONE',  ( -7.157118525848868984, 144.2648164810658216, 276.0058078322479673 ) ) ;
#4281=LINE ( 'NONE', #13158, #6974 ) ;
#4297=FACE_OUTER_BOUND ( 'NONE', #14760, .T. ) ;
#4317=CYLINDRICAL_SURFACE ( 'NONE', #1118, 7.500000000000002665 ) ;
#4336=LINE ( 'NONE', #6079, #21118 ) ;
#4340=ORIENTED_EDGE ( 'NONE', *, *, #9653, .F. ) ;
#4362=CYLINDRICAL_SURFACE ( 'NONE', #11424, 4.200000000000005507 ) ;
#4387=CARTESIAN_POINT ( 'NONE',  ( -41.59559178524079215, 173.5443433241884179, 269.1433480140178744 ) ) ;
#4403=EDGE_CURVE ( 'NONE', #6995, #8963, #6337, .T. ) ;
#4437=ADVANCED_FACE ( 'NONE', ( #19664, #19339 ), #12696, .T. ) ;
#4460=EDGE_CURVE ( 'NONE', #7165, #9573, #10426, .T. ) ;
#4483=VECTOR ( 'NONE', #4639, 1000.000000000000227 ) ;
#4507=EDGE_CURVE ( 'NONE', #12879, #1725, #7386, .T. ) ;
#4534=CARTESIAN_POINT ( 'NONE',  ( 13.04156242531480991, 188.9519362114520220, 275.7250501837552861 ) ) ;
#4544=EDGE_LOOP ( 'NONE', ( #14404, #10765, #20683, #727 ) ) ;
#4545=DIRECTION ( 'NONE',  ( 0.009760756503427210282, -0.9999378516499566327, 0.005387065077606872227 ) ) ;
#4569=CARTESIAN_POINT ( 'NONE',  ( 21.07318851263119441, 147.3427684080706115, 276.4785941130655829 ) ) ;
#4580=LINE ( 'NONE', #13012, #9122 ) ;
#4585=AXIS2_PLACEMENT_3D ( 'NONE', #14722, #808, #2521 ) ;
#4591=EDGE_CURVE ( 'NONE', #14146, #15447, #4580, .T. ) ;
#4604=EDGE_LOOP ( 'NONE', ( #2206, #1422, #13239, #5708 ) ) ;
#4619=CARTESIAN_POINT ( 'NONE',  ( 3.316611465012865967, 166.4147053302257007, 256.5999727791399323 ) ) ;
#4621=ORIENTED_EDGE ( 'NONE', *, *, #10061, .F. ) ;
#4627=CARTESIAN_POINT ( 'NONE',  ( -6.127092384110496504, 143.9207436052761011, 275.8026882763405183 ) ) ;
#4639=DIRECTION ( 'NONE',  ( -0.9726991065672921932, -0.2316562896908778701, 0.01384960395994898341 ) ) ;
#4642=CARTESIAN_POINT ( 'NONE',  ( 16.06222704467468176, 187.3778571219613127, 276.4007913481239029 ) ) ;
#4677=ORIENTED_EDGE ( 'NONE', *, *, #6844, .F. ) ;
#4726=CARTESIAN_POINT ( 'NONE',  ( -14.07506098016042095, 147.3047514226848023, 276.9331026295720335 ) ) ;
#4727=EDGE_CURVE ( 'NONE', #8741, #17624, #3334, .T. ) ;
#4734=CARTESIAN_POINT ( 'NONE',  ( -9.262501379667067880, 187.9054813056602029, 276.0764209250423278 ) ) ;
#4745=CARTESIAN_POINT ( 'NONE',  ( 16.00248264617906457, 188.1407795356557529, 275.7525171823001529 ) ) ;
#4761=CARTESIAN_POINT ( 'NONE',  ( -6.335846763728186559, 188.7674449536879706, 275.9742639064239142 ) ) ;
#4766=VECTOR ( 'NONE', #1983, 999.9999999999998863 ) ;
#4767=PRODUCT_DEFINITION_FORMATION_WITH_SPECIFIED_SOURCE ( 'ANY', '', #5858, .NOT_KNOWN. ) ;
#4773=DIRECTION ( 'NONE',  ( -0.009760756503428009989, 0.9999378516499564107, -0.005387065077611111891 ) ) ;
#4798=VERTEX_POINT ( 'NONE', #19368 ) ;
#4854=CARTESIAN_POINT ( 'NONE',  ( -9.985275337145829155, 186.6414244315945155, 277.9386990328198408 ) ) ;
#4865=CARTESIAN_POINT ( 'NONE',  ( 18.37741161651380395, 185.7965308539349110, 276.6192911305356574 ) ) ;
#4881=AXIS2_PLACEMENT_3D ( 'NONE', #11565, #21862, #1949 ) ;
#4899=FACE_OUTER_BOUND ( 'NONE', #7195, .T. ) ;
#4903=AXIS2_PLACEMENT_3D ( 'NONE', #18282, #599, #3910 ) ;
#4914=EDGE_CURVE ( 'NONE', #16716, #17834, #1261, .T. ) ;
#4976=DIRECTION ( 'NONE',  ( 0.009760756503428003050, -0.9999378516499565217, 0.005387065077610373766 ) ) ;
#4986=EDGE_CURVE ( 'NONE', #2150, #14146, #6216, .T. ) ;
#5004=CARTESIAN_POINT ( 'NONE',  ( 3.316624388958365088, 166.4147108432491109, 256.6009726804241495 ) ) ;
#5017=DIRECTION ( 'NONE',  ( 0.9726991065672923042, 0.2316562896908778701, -0.01384960395994898341 ) ) ;
#5040=EDGE_CURVE ( 'NONE', #11316, #8236, #8413, .T. ) ;
#5067=CARTESIAN_POINT ( 'NONE',  ( -8.178437098313294129, 145.2910952780770515, 277.6650327932460414 ) ) ;
#5071=CIRCLE ( 'NONE', #8012, 24.23418050574097293 ) ;
#5075=CARTESIAN_POINT ( 'NONE',  ( 48.64240681911486774, 159.4614951111008452, 276.0554384422054000 ) ) ;
#5083=DIRECTION ( 'NONE',  ( -0.9998688410312766006, -0.009690170827377751067, 0.01297695357578096571 ) ) ;
#5107=CARTESIAN_POINT ( 'NONE',  ( 14.28940378674282208, 144.6940418464262166, 276.8225175484434999 ) ) ;
#5116=CARTESIAN_POINT ( 'NONE',  ( -41.52238611146507452, 166.0448094368137504, 269.1837510020998820 ) ) ;
#5134=DIRECTION ( 'NONE',  ( -0.9726991065672923042, -0.2316562896908775926, 0.01384960395994898341 ) ) ;
#5135=ADVANCED_FACE ( 'NONE', ( #18326 ), #22172, .F. ) ;
#5141=DIRECTION ( 'NONE',  ( 0.009760756503427210282, -0.9999378516499566327, 0.005387065077606872227 ) ) ;
#5149=ORIENTED_EDGE ( 'NONE', *, *, #2216, .F. ) ;
#5159=CARTESIAN_POINT ( 'NONE',  ( 13.18868299908003294, 189.1369543048038224, 275.2921301635565214 ) ) ;
#5167=EDGE_LOOP ( 'NONE', ( #10414, #4621, #6636 ) ) ;
#5178=CARTESIAN_POINT ( 'NONE',  ( -13.50073983619024176, 183.7065926015648074, 278.6553669534396249 ) ) ;
#5180=LINE ( 'NONE', #14282, #18967 ) ;
#5197=CIRCLE ( 'NONE', #3393, 7.999999999999985789 ) ;
#5219=EDGE_CURVE ( 'NONE', #5976, #11327, #12335, .T. ) ;
#5251=VERTEX_POINT ( 'NONE', #256 ) ;
#5294=EDGE_LOOP ( 'NONE', ( #8723, #16544 ) ) ;
#5305=DIRECTION ( 'NONE',  ( 0.009760756503428011724, -0.9999378516499566327, 0.005387065077610982654 ) ) ;
#5342=DIRECTION ( 'NONE',  ( -0.9726991065672923042, -0.2316562896908775926, 0.01384960395994898341 ) ) ;
#5345=ORIENTED_EDGE ( 'NONE', *, *, #406, .F. ) ;
#5347=DIRECTION ( 'NONE',  ( -0.01292394549866738608, -0.005513023399720468239, -0.9999012842304692006 ) ) ;
#5354=EDGE_CURVE ( 'NONE', #5504, #8741, #15422, .T. ) ;
#5365=DIRECTION ( 'NONE',  ( 0.009760756503427111402, -0.9999378516499564107, 0.005387065077611765014 ) ) ;
#5397=CARTESIAN_POINT ( 'NONE',  ( 17.25791503114635361, 186.5747366875307875, 277.7312368246228971 ) ) ;
#5446=AXIS2_PLACEMENT_3D ( 'NONE', #1468, #6625, #15496 ) ;
#5451=LINE ( 'NONE', #21425, #19559 ) ;
#5485=DIRECTION ( 'NONE',  ( 0.01292394549866738955, 0.005513023399720468239, 0.9999012842304693116 ) ) ;
#5493=CARTESIAN_POINT ( 'NONE',  ( 48.46580958134982353, 166.9169248112777666, 268.0158251802795917 ) ) ;
#5504=VERTEX_POINT ( 'NONE', #12858 ) ;
#5508=ORIENTED_EDGE ( 'NONE', *, *, #72, .F. ) ;
#5562=CARTESIAN_POINT ( 'NONE',  ( -41.41899454747574083, 166.0889136240115249, 277.1829612759436827 ) ) ;
#5620=ORIENTED_EDGE ( 'NONE', *, *, #1256, .F. ) ;
#5639=CARTESIAN_POINT ( 'NONE',  ( 3.316624388958365088, 166.4147108432491109, 256.6009726804241495 ) ) ;
#5676=VERTEX_POINT ( 'NONE', #2954 ) ;
#5686=FACE_OUTER_BOUND ( 'NONE', #9770, .T. ) ;
#5708=ORIENTED_EDGE ( 'NONE', *, *, #20157, .T. ) ;
#5768=ADVANCED_FACE ( 'NONE', ( #4899 ), #10427, .F. ) ;
#5770=CARTESIAN_POINT ( 'NONE',  ( 11.33842039275930347, 189.5802358106135159, 275.5617015998586794 ) ) ;
#5798=ADVANCED_FACE ( 'NONE', ( #17201 ), #22342, .T. ) ;
#5821=CARTESIAN_POINT ( 'NONE',  ( -44.49988481842636645, 152.0384941537814427, 275.3698588368105789 ) ) ;
#5858=PRODUCT ( 'Flange', 'Flange', '', ( #2974 ) ) ;
#5877=ORIENTED_EDGE ( 'NONE', *, *, #7864, .F. ) ;
#5902=AXIS2_PLACEMENT_3D ( 'NONE', #7594, #21582, #9886 ) ;
#5924=CARTESIAN_POINT ( 'NONE',  ( 3.238525412985443275, 174.4142081434253555, 256.5568762585190257 ) ) ;
#5958=CARTESIAN_POINT ( 'NONE',  ( 8.633533809377718526, 190.8419313418282854, 256.3975693155348381 ) ) ;
#5976=VERTEX_POINT ( 'NONE', #7641 ) ;
#6056=DIRECTION ( 'NONE',  ( 0.01292394549866738955, 0.005513023399720468239, 0.9999012842304693116 ) ) ;
#6079=CARTESIAN_POINT ( 'NONE',  ( -2.096375399687118168, 190.2200455327031534, 274.6112675210154634 ) ) ;
#6108=ADVANCED_BREP_SHAPE_REPRESENTATION ( '', ( #2374, #6292 ), #21305 ) ;
#6123=VERTEX_POINT ( 'NONE', #20952 ) ;
#6133=ORIENTED_EDGE ( 'NONE', *, *, #20759, .F. ) ;
#6154=CARTESIAN_POINT ( 'NONE',  ( -44.07569325658431580, 153.9910965579657613, 275.2838043771024559 ) ) ;
#6156=DIRECTION ( 'NONE',  ( 0.01292394549866738782, 0.005513023399720468239, 0.9999012842304692006 ) ) ;
#6164=CARTESIAN_POINT ( 'NONE',  ( 48.61019632265355028, 162.7612900215456762, 276.0376611274493257 ) ) ;
#6196=EDGE_CURVE ( 'NONE', #8063, #20449, #1128, .T. ) ;
#6197=CIRCLE ( 'NONE', #14672, 4.200000000000005507 ) ;
#6214=CARTESIAN_POINT ( 'NONE',  ( -9.322685960893931423, 145.0715325292690920, 276.3947491604697007 ) ) ;
#6216=CIRCLE ( 'NONE', #3263, 24.99999999999998224 ) ;
#6224=( NAMED_UNIT ( * ) SI_UNIT ( $, .STERADIAN. ) SOLID_ANGLE_UNIT ( ) );
#6229=ORIENTED_EDGE ( 'NONE', *, *, #9098, .F. ) ;
#6242=CARTESIAN_POINT ( 'NONE',  ( 9.260057161142448479, 190.1982426752826143, 274.6915518483514234 ) ) ;
#6244=DIRECTION ( 'NONE',  ( 0.9726991065672921932, 0.2316562896908778701, -0.01384960395994898168 ) ) ;
#6255=ORIENTED_EDGE ( 'NONE', *, *, #3114, .T. ) ;
#6284=CARTESIAN_POINT ( 'NONE',  ( 51.60019979106836985, 180.9901659820745294, 273.9681169626219344 ) ) ;
#6292=AXIS2_PLACEMENT_3D ( 'NONE', #3102, #12069, #1395 ) ;
#6294=EDGE_CURVE ( 'NONE', #6123, #16406, #4281, .T. ) ;
#6314=VERTEX_POINT ( 'NONE', #14783 ) ;
#6319=DIRECTION ( 'NONE',  ( 0.009760756503427876415, -0.9999378516499564107, 0.005387065077611007807 ) ) ;
#6337=LINE ( 'NONE', #16906, #16840 ) ;
#6367=AXIS2_PLACEMENT_3D ( 'NONE', #13744, #13515, #2825 ) ;
#6372=CARTESIAN_POINT ( 'NONE',  ( -1.632550740186645921, 142.7036636415817838, 274.8672572718562037 ) ) ;
#6377=DIRECTION ( 'NONE',  ( 0.009760756503428009989, -0.9999378516499564107, 0.005387065077611111891 ) ) ;
#6380=CARTESIAN_POINT ( 'NONE',  ( -10.44786468173362337, 186.3147661259626204, 278.0874267879351009 ) ) ;
#6384=AXIS2_PLACEMENT_3D ( 'NONE', #18329, #6156, #8940 ) ;
#6385=VERTEX_POINT ( 'NONE', #16494 ) ;
#6388=AXIS2_PLACEMENT_3D ( 'NONE', #13952, #12465, #8883 ) ;
#6405=ORIENTED_EDGE ( 'NONE', *, *, #4986, .F. ) ;
#6415=ADVANCED_FACE ( 'NONE', ( #3022 ), #12070, .F. ) ;
#6430=CARTESIAN_POINT ( 'NONE',  ( 11.42559457476033025, 143.4049563503333786, 275.1388332802161472 ) ) ;
#6448=LINE ( 'NONE', #11506, #158 ) ;
#6449=ORIENTED_EDGE ( 'NONE', *, *, #9115, .T. ) ;
#6482=CARTESIAN_POINT ( 'NONE',  ( -8.417507809094315618, 145.3803201924227153, 276.8538022553906899 ) ) ;
#6488=CARTESIAN_POINT ( 'NONE',  ( -9.289650516680991288, 187.1478790530904348, 276.7252570793428390 ) ) ;
#6500=CARTESIAN_POINT ( 'NONE',  ( 16.79060435579898325, 186.8892895049134779, 277.5964890151019517 ) ) ;
#6517=CARTESIAN_POINT ( 'NONE',  ( 11.46456758449441971, 143.4062123375417457, 275.1480316732433948 ) ) ;
#6544=DIRECTION ( 'NONE',  ( -0.9770372205688160339, 0.2127605332646582970, 0.01145535281434409587 ) ) ;
#6546=ORIENTED_EDGE ( 'NONE', *, *, #5354, .T. ) ;
#6582=CARTESIAN_POINT ( 'NONE',  ( -3.813579275066386387, 143.2905249558850755, 275.5763592733787277 ) ) ;
#6584=B_SPLINE_CURVE_WITH_KNOTS ( 'NONE', 3,
 ( #9051, #17836, #16105, #21234, #14260, #14386, #2072, #7465, #12656, #12531, #7577, #14501, #19628, #3896, #10913, #17936 ),
 .UNSPECIFIED., .F., .F.,
 ( 4, 2, 2, 2, 2, 2, 2, 4 ),
 ( -3.123367963890199151E-05, 0.001725203944011580084, 0.003481641567662062051, 0.006994516814963025984, 0.008750954438613504915, 0.01050739206226398471, 0.01226382968591446451, 0.01402026730956494605 ),
 .UNSPECIFIED. ) ;
#6588=CARTESIAN_POINT ( 'NONE',  ( -7.645763215668887725, 188.5431871033221967, 275.7782546341398984 ) ) ;
#6593=VECTOR ( 'NONE', #16228, 1000.000000000000000 ) ;
#6599=DIRECTION ( 'NONE',  ( 0.9726991065672921932, 0.2316562896908778701, -0.01384960395994898168 ) ) ;
#6610=DIRECTION ( 'NONE',  ( -0.009760756503428009989, 0.9999378516499564107, -0.005387065077611111891 ) ) ;
#6625=DIRECTION ( 'NONE',  ( 0.01292394549866738782, 0.005513023399720468239, 0.9999012842304692006 ) ) ;
#6626=CARTESIAN_POINT ( 'NONE',  ( 13.46976562096918606, 144.2755497367511452, 275.9635810563158316 ) ) ;
#6636=ORIENTED_EDGE ( 'NONE', *, *, #2926, .F. ) ;
#6655=ORIENTED_EDGE ( 'NONE', *, *, #6996, .T. ) ;
#6657=CARTESIAN_POINT ( 'NONE',  ( -44.49988481842637356, 152.0384941537814427, 275.3698588368105789 ) ) ;
#6658=ORIENTED_EDGE ( 'NONE', *, *, #15764, .F. ) ;
#6673=DIRECTION ( 'NONE',  ( -0.2120957809210262945, -0.9763012020921555401, 0.04302722985403674427 ) ) ;
#6679=EDGE_CURVE ( 'NONE', #7165, #164, #401, .T. ) ;
#6692=EDGE_CURVE ( 'NONE', #15161, #11316, #12877, .T. ) ;
#6698=CARTESIAN_POINT ( 'NONE',  ( -10.32470579490272833, 146.5997690630838406, 277.1622549925964449 ) ) ;
#6705=DIRECTION ( 'NONE',  ( -0.01292394549866738782, -0.005513023399720468239, -0.9999012842304692006 ) ) ;
#6718=CARTESIAN_POINT ( 'NONE',  ( 15.83726170982532544, 187.4852378640612756, 277.2946379115891204 ) ) ;
#6724=CARTESIAN_POINT ( 'NONE',  ( -41.49220022125144425, 173.5884475113861924, 277.1425582878616183 ) ) ;
#6749=CARTESIAN_POINT ( 'NONE',  ( 16.87037639224499586, 145.3228975761790025, 276.0538200153999924 ) ) ;
#6750=CARTESIAN_POINT ( 'NONE',  ( 48.46580958134982353, 166.9169248112777666, 268.0158251802795917 ) ) ;
#6793=ORIENTED_EDGE ( 'NONE', *, *, #10206, .F. ) ;
#6796=DIRECTION ( 'NONE',  ( -0.009760756503428008254, 0.9999378516499564107, -0.005387065077611006073 ) ) ;
#6800=CARTESIAN_POINT ( 'NONE',  ( -7.125252400461968172, 188.3623996986441682, 276.8553851557323355 ) ) ;
#6835=ORIENTED_EDGE ( 'NONE', *, *, #5354, .F. ) ;
#6843=CARTESIAN_POINT ( 'NONE',  ( 17.16844361279197884, 146.4225787965282279, 277.8094805302229702 ) ) ;
#6844=EDGE_CURVE ( 'NONE', #13521, #10577, #1174, .T. ) ;
#6884=CARTESIAN_POINT ( 'NONE',  ( 8.732865712828665750, 190.3249964942741883, 274.4707185275763095 ) ) ;
#6934=CARTESIAN_POINT ( 'NONE',  ( 3.807734317907725430, 166.6242057324384689, 294.5972214811819754 ) ) ;
#6950=AXIS2_PLACEMENT_3D ( 'NONE', #5004, #13986, #4773 ) ;
#6955=CARTESIAN_POINT ( 'NONE',  ( 16.44176152114187417, 145.9028759403760205, 276.6200799972182836 ) ) ;
#6956=ORIENTED_EDGE ( 'NONE', *, *, #21695, .F. ) ;
#6962=EDGE_CURVE ( 'NONE', #10899, #20552, #16951, .T. ) ;
#6974=VECTOR ( 'NONE', #9813, 999.9999999999998863 ) ;
#6975=AXIS2_PLACEMENT_3D ( 'NONE', #19435, #22620, #5305 ) ;
#6991=DIRECTION ( 'NONE',  ( 0.01292394549866738782, 0.005513023399720468239, 0.9999012842304692006 ) ) ;
#6995=VERTEX_POINT ( 'NONE', #6284 ) ;
#6996=EDGE_CURVE ( 'NONE', #1331, #11181, #2727, .T. ) ;
#7039=DIRECTION ( 'NONE',  ( 0.01292394549866738782, 0.005513023399720468239, 0.9999012842304692006 ) ) ;
#7051=CARTESIAN_POINT ( 'NONE',  ( 3.833582208905060185, 166.6352317792379267, 296.5970240496429255 ) ) ;
#7066=ORIENTED_EDGE ( 'NONE', *, *, #4914, .F. ) ;
#7103=VECTOR ( 'NONE', #6544, 999.9999999999998863 ) ;
#7110=ORIENTED_EDGE ( 'NONE', *, *, #14162, .T. ) ;
#7129=EDGE_CURVE ( 'NONE', #15161, #15824, #15858, .T. ) ;
#7148=LINE ( 'NONE', #12437, #4766 ) ;
#7165=VERTEX_POINT ( 'NONE', #16381 ) ;
#7168=CARTESIAN_POINT ( 'NONE',  ( 3.833582208905060185, 166.6352317792379267, 296.5970240496429255 ) ) ;
#7181=DIRECTION ( 'NONE',  ( 0.009760756503427813965, -0.9999378516499565217, 0.005387065077607405654 ) ) ;
#7190=DIRECTION ( 'NONE',  ( 0.009760756503428008254, -0.9999378516499564107, 0.005387065077611006073 ) ) ;
#7195=EDGE_LOOP ( 'NONE', ( #3972, #425, #20651, #1549 ) ) ;
#7196=CARTESIAN_POINT ( 'NONE',  ( 4.039679098813819813, 142.9554882982450010, 294.7945285032504330 ) ) ;
#7268=ORIENTED_EDGE ( 'NONE', *, *, #10061, .T. ) ;
#7284=DIRECTION ( 'NONE',  ( 0.01292394549866738782, 0.005513023399720468239, 0.9999012842304692006 ) ) ;
#7288=ORIENTED_EDGE ( 'NONE', *, *, #9115, .F. ) ;
#7297=ORIENTED_EDGE ( 'NONE', *, *, #22451, .T. ) ;
#7307=AXIS2_PLACEMENT_3D ( 'NONE', #20528, #11492, #6319 ) ;
#7347=ORIENTED_EDGE ( 'NONE', *, *, #4727, .T. ) ;
#7349=ORIENTED_EDGE ( 'NONE', *, *, #20498, .F. ) ;
#7386=LINE ( 'NONE', #7512, #20496 ) ;
#7411=ORIENTED_EDGE ( 'NONE', *, *, #388, .T. ) ;
#7422=DIRECTION ( 'NONE',  ( 0.01292394549866738782, 0.005513023399720468239, 0.9999012842304692006 ) ) ;
#7432=VERTEX_POINT ( 'NONE', #21036 ) ;
#7452=CIRCLE ( 'NONE', #130, 4.200000000000005507 ) ;
#7456=EDGE_LOOP ( 'NONE', ( #12336, #5508, #2027, #9177 ) ) ;
#7458=CARTESIAN_POINT ( 'NONE',  ( -2.616420304248261886, 190.0885906883363816, 274.8459139047729423 ) ) ;
#7465=CARTESIAN_POINT ( 'NONE',  ( 15.73089101666271361, 145.5050201865991539, 277.3435683618253620 ) ) ;
#7491=FACE_OUTER_BOUND ( 'NONE', #4544, .T. ) ;
#7492=PRODUCT_DEFINITION ( 'UNKNOWN', '', #4767, #15494 ) ;
#7512=CARTESIAN_POINT ( 'NONE',  ( 8.633533809377713197, 190.8419313418282854, 256.3975693155348381 ) ) ;
#7517=CARTESIAN_POINT ( 'NONE',  ( 12.86429881287754284, 189.0102787272791716, 276.1886381430309143 ) ) ;
#7531=CYLINDRICAL_SURFACE ( 'NONE', #20705, 2.000000000000003997 ) ;
#7568=ORIENTED_EDGE ( 'NONE', *, *, #7964, .F. ) ;
#7577=CARTESIAN_POINT ( 'NONE',  ( 17.62523603308973463, 146.7439693644061265, 277.9400347667066171 ) ) ;
#7594=CARTESIAN_POINT ( 'NONE',  ( 3.600951189929047391, 166.5359973580429482, 278.5988009334944877 ) ) ;
#7618=CARTESIAN_POINT ( 'NONE',  ( 48.50680475866421659, 162.7171858343479016, 268.0384508536055819 ) ) ;
#7640=DIRECTION ( 'NONE',  ( 0.01292394549866738955, 0.005513023399720468239, 0.9999012842304693116 ) ) ;
#7641=CARTESIAN_POINT ( 'NONE',  ( -41.44918043768936400, 158.5452755494390544, 269.2241539901819465 ) ) ;
#7667=LINE ( 'NONE', #18251, #14064 ) ;
#7701=CARTESIAN_POINT ( 'NONE',  ( 8.306869994213354147, 188.3716244831220479, 274.4171887809970940 ) ) ;
#7711=DIRECTION ( 'NONE',  ( 0.009760756503428008254, -0.9999378516499564107, 0.005387065077611006073 ) ) ;
#7713=DIRECTION ( 'NONE',  ( 0.009760756503428037745, -0.9999378516499562997, 0.005387065077612779827 ) ) ;
#7736=CARTESIAN_POINT ( 'NONE',  ( -4.313798532395376917, 189.6286013151541283, 275.0874112264361884 ) ) ;
#7740=CARTESIAN_POINT ( 'NONE',  ( 19.50026166618112100, 184.8320841190834756, 278.1813969851201023 ) ) ;
#7763=DIRECTION ( 'NONE',  ( 0.01292394549866738608, 0.005513023399720468239, 0.9999012842304692006 ) ) ;
#7864=EDGE_CURVE ( 'NONE', #7432, #20838, #95, .T. ) ;
#7881=CARTESIAN_POINT ( 'NONE',  ( 9.839100211760563042, 190.0747034078442539, 274.8007098013740688 ) ) ;
#7902=CARTESIAN_POINT ( 'NONE',  ( -41.67747345744908216, 165.9786531560170886, 257.1849355913342379 ) ) ;
#7903=ORIENTED_EDGE ( 'NONE', *, *, #22451, .F. ) ;
#7920=SHAPE_DEFINITION_REPRESENTATION ( #19981, #21177 ) ;
#7947=SURFACE_STYLE_FILL_AREA ( #8054 ) ;
#7953=CARTESIAN_POINT ( 'NONE',  ( 48.54335325434182380, 166.9500029516760833, 274.0152328856624422 ) ) ;
#7964=EDGE_CURVE ( 'NONE', #16920, #1331, #12582, .T. ) ;
#7980=CARTESIAN_POINT ( 'NONE',  ( 10.93157627012523214, 189.7456778768155061, 275.1296412434647323 ) ) ;
#7981=ORIENTED_EDGE ( 'NONE', *, *, #4914, .T. ) ;
#7994=DIRECTION ( 'NONE',  ( 0.7056475024472779189, -0.7085438702141405587, -0.005214045635221192972 ) ) ;
#8012=AXIS2_PLACEMENT_3D ( 'NONE', #14890, #11412, #18424 ) ;
#8032=CARTESIAN_POINT ( 'NONE',  ( 48.46580958134982353, 166.9169248112777666, 268.0158251802795917 ) ) ;
#8054=FILL_AREA_STYLE ('',( #2790 ) ) ;
#8063=VERTEX_POINT ( 'NONE', #19615 ) ;
#8089=CARTESIAN_POINT ( 'NONE',  ( -12.66072403271054903, 184.5155800142387363, 278.5994379001652987 ) ) ;
#8093=ADVANCED_FACE ( 'NONE', ( #16091 ), #3885, .F. ) ;
#8103=EDGE_CURVE ( 'NONE', #11316, #164, #17700, .T. ) ;
#8106=CARTESIAN_POINT ( 'NONE',  ( 21.22526757802852515, 185.7451911998024343, 276.2648941004949847 ) ) ;
#8129=AXIS2_PLACEMENT_3D ( 'NONE', #2109, #9100, #12578 ) ;
#8143=EDGE_LOOP ( 'NONE', ( #20766, #1644 ) ) ;
#8149=ORIENTED_EDGE ( 'NONE', *, *, #4727, .F. ) ;
#8207=AXIS2_PLACEMENT_3D ( 'NONE', #1447, #10065, #4976 ) ;
#8209=EDGE_CURVE ( 'NONE', #8963, #1725, #7667, .T. ) ;
#8213=CARTESIAN_POINT ( 'NONE',  ( -12.43529986855201486, 186.4710608878919516, 276.5579441034727779 ) ) ;
#8225=DIRECTION ( 'NONE',  ( 0.01292394549866738955, 0.005513023399720468239, 0.9999012842304693116 ) ) ;
#8236=VERTEX_POINT ( 'NONE', #5821 ) ;
#8245=AXIS2_PLACEMENT_3D ( 'NONE', #11857, #18619, #14973 ) ;
#8275=ADVANCED_FACE ( 'NONE', ( #678 ), #17631, .T. ) ;
#8284=ORIENTED_EDGE ( 'NONE', *, *, #20592, .T. ) ;
#8306=CARTESIAN_POINT ( 'NONE',  ( -10.07101741848119936, 146.4908573800363456, 278.3054745090071833 ) ) ;
#8310=CARTESIAN_POINT ( 'NONE',  ( -9.043880562332304862, 187.2595245844938177, 277.6087870137185973 ) ) ;
#8338=CARTESIAN_POINT ( 'NONE',  ( 13.30359063182643808, 144.2231605954833924, 276.4307627107033341 ) ) ;
#8388=SURFACE_STYLE_USAGE ( .BOTH. , #14977 ) ;
#8413=CIRCLE ( 'NONE', #10249, 2.000000000000003997 ) ;
#8429=DIRECTION ( 'NONE',  ( 0.01292394549866738955, 0.005513023399720468239, 0.9999012842304693116 ) ) ;
#8448=AXIS2_PLACEMENT_3D ( 'NONE', #1684, #19118, #6610 ) ;
#8449=ORIENTED_EDGE ( 'NONE', *, *, #11190, .T. ) ;
#8472=CARTESIAN_POINT ( 'NONE',  ( -14.56978029430814026, 147.5825162344054888, 276.9379655111616785 ) ) ;
#8483=SHAPE_REPRESENTATION_RELATIONSHIP ( 'NONE' , 'NONE' ,  #21177, #6108 ) ;
#8504=ORIENTED_EDGE ( 'NONE', *, *, #4403, .T. ) ;
#8519=CARTESIAN_POINT ( 'NONE',  ( -6.151324038728556154, 188.8277583064068779, 276.4336127016060800 ) ) ;
#8523=CARTESIAN_POINT ( 'NONE',  ( -11.42851267050998132, 147.5070834042510342, 278.6502049059965884 ) ) ;
#8531=CIRCLE ( 'NONE', #15532, 14.36898871458905269 ) ;
#8545=CARTESIAN_POINT ( 'NONE',  ( 3.577593693774890227, 190.2936927735998154, 294.5394986654007994 ) ) ;
#8555=AXIS2_PLACEMENT_3D ( 'NONE', #15301, #3094, #5365 ) ;
#8585=ORIENTED_EDGE ( 'NONE', *, *, #16391, .F. ) ;
#8630=ADVANCED_FACE ( 'NONE', ( #18339 ), #11681, .F. ) ;
#8631=EDGE_CURVE ( 'NONE', #19271, #6314, #21277, .T. ) ;
#8647=CARTESIAN_POINT ( 'NONE',  ( 4.019267399398602336, 144.9537609278173704, 294.7139688332605374 ) ) ;
#8668=CARTESIAN_POINT ( 'NONE',  ( 17.85676077817555552, 146.8644376350167420, 276.7956092302854358 ) ) ;
#8686=CARTESIAN_POINT ( 'NONE',  ( 8.732651047105484565, 144.7526087692596946, 274.6521818617012514 ) ) ;
#8723=ORIENTED_EDGE ( 'NONE', *, *, #15764, .T. ) ;
#8741=VERTEX_POINT ( 'NONE', #14694 ) ;
#8746=ADVANCED_FACE ( 'NONE', ( #12129 ), #3685, .T. ) ;
#8751=CARTESIAN_POINT ( 'NONE',  ( -2.153876626942607952, 142.8329195585684488, 275.1002313843466709 ) ) ;
#8779=PLANE ( 'NONE',  #15194 ) ;
#8837=AXIS2_PLACEMENT_3D ( 'NONE', #13397, #15000, #13161 ) ;
#8852=PLANE ( 'NONE',  #2789 ) ;
#8883=DIRECTION ( 'NONE',  ( 0.009760756503427210282, -0.9999378516499566327, 0.005387065077606872227 ) ) ;
#8906=CARTESIAN_POINT ( 'NONE',  ( 48.56920114533915722, 166.9610289984755127, 276.0150354541233924 ) ) ;
#8922=EDGE_LOOP ( 'NONE', ( #16547, #17610, #17184 ) ) ;
#8940=DIRECTION ( 'NONE',  ( 0.009760756503428037745, -0.9999378516499566327, 0.005387065077611006073 ) ) ;
#8957=CIRCLE ( 'NONE', #21777, 1.999999999999997558 ) ;
#8963=VERTEX_POINT ( 'NONE', #10521 ) ;
#8983=DIRECTION ( 'NONE',  ( 0.009760756503428004785, -0.9999378516499564107, 0.005387065077611765014 ) ) ;
#8996=CARTESIAN_POINT ( 'NONE',  ( -2.673171722481940016, 142.9732003400563656, 275.3325226564539889 ) ) ;
#9031=PLANE ( 'NONE',  #9242 ) ;
#9045=CARTESIAN_POINT ( 'NONE',  ( -9.034450215842609211, 187.2654037237712146, 277.6052983116423434 ) ) ;
#9051=CARTESIAN_POINT ( 'NONE',  ( 9.196690372329049623, 142.8086146031528187, 274.7267082784170498 ) ) ;
#9055=CARTESIAN_POINT ( 'NONE',  ( 20.69463332847445614, 186.0431207901125674, 276.2701100107056504 ) ) ;
#9063=EDGE_CURVE ( 'NONE', #345, #5676, #14364, .T. ) ;
#9068=FACE_OUTER_BOUND ( 'NONE', #13927, .T. ) ;
#9089=ORIENTED_EDGE ( 'NONE', *, *, #6844, .T. ) ;
#9098=EDGE_CURVE ( 'NONE', #13090, #16716, #22391, .T. ) ;
#9100=DIRECTION ( 'NONE',  ( -0.9726991065672926373, -0.2316562896908763991, 0.01384960395994897994 ) ) ;
#9106=COLOUR_RGB ( '', 0.08235294, 0.09019608, 0.10196078) ;
#9115=EDGE_CURVE ( 'NONE', #11327, #20863, #790, .T. ) ;
#9122=VECTOR ( 'NONE', #16689, 1000.000000000000227 ) ;
#9125=ORIENTED_EDGE ( 'NONE', *, *, #19887, .T. ) ;
#9160=CARTESIAN_POINT ( 'NONE',  ( -1.182511287347259854, 144.6672920925655319, 276.7810053806090309 ) ) ;
#9164=EDGE_LOOP ( 'NONE', ( #7110, #90, #3636, #11129 ) ) ;
#9177=ORIENTED_EDGE ( 'NONE', *, *, #388, .F. ) ;
#9183=CIRCLE ( 'NONE', #6975, 24.23418050574097293 ) ;
#9216=VECTOR ( 'NONE', #6056, 999.9999999999998863 ) ;
#9242=AXIS2_PLACEMENT_3D ( 'NONE', #21110, #14006, #5134 ) ;
#9265=DIRECTION ( 'NONE',  ( -0.009760756503428008254, 0.9999378516499565217, -0.005387065077611300108 ) ) ;
#9266=EDGE_LOOP ( 'NONE', ( #18337, #6658, #17075, #15334 ) ) ;
#9269=AXIS2_PLACEMENT_3D ( 'NONE', #20538, #19164, #3437 ) ;
#9314=PLANE ( 'NONE',  #9758 ) ;
#9326=ORIENTED_EDGE ( 'NONE', *, *, #10855, .T. ) ;
#9329=AXIS2_PLACEMENT_3D ( 'NONE', #19691, #5347, #17902 ) ;
#9353=DIRECTION ( 'NONE',  ( 0.009760756503428037745, -0.9999378516499562997, 0.005387065077612779827 ) ) ;
#9386=TOROIDAL_SURFACE ( 'NONE', #22203, 26.23296215977915935, 2.000000000000000000 ) ;
#9404=FACE_OUTER_BOUND ( 'NONE', #12860, .T. ) ;
#9421=CYLINDRICAL_SURFACE ( 'NONE', #4903, 2.000000000000008438 ) ;
#9424=ORIENTED_EDGE ( 'NONE', *, *, #15604, .T. ) ;
#9448=CARTESIAN_POINT ( 'NONE',  ( -3.208759309630397460, 189.9379666734643592, 274.8508292759004235 ) ) ;
#9454=CARTESIAN_POINT ( 'NONE',  ( 19.93494142535458025, 184.4443040380761829, 278.2191359478135269 ) ) ;
#9536=ORIENTED_EDGE ( 'NONE', *, *, #15974, .F. ) ;
#9542=CARTESIAN_POINT ( 'NONE',  ( 51.50086788761742440, 181.5071008296286266, 255.8949677505804061 ) ) ;
#9573=VERTEX_POINT ( 'NONE', #18981 ) ;
#9596=ORIENTED_EDGE ( 'NONE', *, *, #14367, .F. ) ;
#9611=CARTESIAN_POINT ( 'NONE',  ( 8.732865712828660421, 190.3249964942741883, 274.4707185275763095 ) ) ;
#9615=CARTESIAN_POINT ( 'NONE',  ( 4.045115290395937535, 144.9647869746168283, 296.7137714017214876 ) ) ;
#9622=CIRCLE ( 'NONE', #22421, 7.500000000000002665 ) ;
#9630=EDGE_CURVE ( 'NONE', #1331, #16920, #15601, .T. ) ;
#9637=CARTESIAN_POINT ( 'NONE',  ( 20.70083805927512088, 149.3646325075532957, 278.4026507072620120 ) ) ;
#9653=EDGE_CURVE ( 'NONE', #10899, #13090, #609, .T. ) ;
#9734=AXIS2_PLACEMENT_3D ( 'NONE', #15790, #7039, #15913 ) ;
#9758=AXIS2_PLACEMENT_3D ( 'NONE', #9542, #21696, #14622 ) ;
#9770=EDGE_LOOP ( 'NONE', ( #7568, #7297, #21008, #3518 ) ) ;
#9778=DIRECTION ( 'NONE',  ( -0.02033837109167977927, -0.03960957306447945164, -0.9990082243820552765 ) ) ;
#9786=CARTESIAN_POINT ( 'NONE',  ( -1.632550740186649252, 142.7036636415817838, 274.8672572718561469 ) ) ;
#9799=EDGE_CURVE ( 'NONE', #6385, #17869, #2398, .T. ) ;
#9813=DIRECTION ( 'NONE',  ( 0.01292394549866738955, 0.005513023399720468239, 0.9999012842304693116 ) ) ;
#9829=CARTESIAN_POINT ( 'NONE',  ( 21.71998689217155487, 185.4674263880815204, 276.2600312189053966 ) ) ;
#9862=CARTESIAN_POINT ( 'NONE',  ( -14.54393240331080506, 147.5935422812049467, 278.9377680796226286 ) ) ;
#9865=CARTESIAN_POINT ( 'NONE',  ( 9.755537514967961954, 142.9459895023150580, 274.8304158214364179 ) ) ;
#9876=DIRECTION ( 'NONE',  ( 0.01292394549866738782, 0.005513023399720468239, 0.9999012842304692006 ) ) ;
#9886=DIRECTION ( 'NONE',  ( 0.009760756503428003050, -0.9999378516499564107, 0.005387065077611006073 ) ) ;
#9898=CARTESIAN_POINT ( 'NONE',  ( -2.476119979858689923, 190.7342627770796355, 256.5417576885990343 ) ) ;
#9899=ORIENTED_EDGE ( 'NONE', *, *, #4403, .F. ) ;
#9947=DIRECTION ( 'NONE',  ( 0.01292394549866738782, 0.005513023399720468239, 0.9999012842304692006 ) ) ;
#9957=DIRECTION ( 'NONE',  ( 0.009760756503427813965, -0.9999378516499565217, 0.005387065077607405654 ) ) ;
#9969=CARTESIAN_POINT ( 'NONE',  ( 9.196690372329099361, 142.8086146031528187, 274.7267082784171066 ) ) ;
#10041=CARTESIAN_POINT ( 'NONE',  ( -3.711637254857439228, 143.2701774585193277, 275.7994991500716537 ) ) ;
#10047=CARTESIAN_POINT ( 'NONE',  ( -11.39723178008673443, 186.9724665881753367, 276.4227300934390996 ) ) ;
#10048=ORIENTED_EDGE ( 'NONE', *, *, #4460, .T. ) ;
#10061=EDGE_CURVE ( 'NONE', #17705, #19271, #6584, .T. ) ;
#10062=CIRCLE ( 'NONE', #10430, 2.000000000000005329 ) ;
#10065=DIRECTION ( 'NONE',  ( 0.01292394549866738782, 0.005513023399720468239, 0.9999012842304692006 ) ) ;
#10066=CARTESIAN_POINT ( 'NONE',  ( 18.62401128910041237, 185.5621796316531231, 278.0519500310857666 ) ) ;
#10072=VERTEX_POINT ( 'NONE', #12757 ) ;
#10080=TOROIDAL_SURFACE ( 'NONE', #16706, 21.67179167071591550, 2.000000000000000000 ) ;
#10089=CARTESIAN_POINT ( 'NONE',  ( 10.29791149212331902, 143.0840241353079421, 275.0539025729775631 ) ) ;
#10096=ADVANCED_FACE ( 'NONE', ( #9404 ), #691, .F. ) ;
#10114=AXIS2_PLACEMENT_3D ( 'NONE', #16359, #11160, #598 ) ;
#10152=CARTESIAN_POINT ( 'NONE',  ( 48.46580958134982353, 166.9169248112777666, 268.0158251802795917 ) ) ;
#10153=CARTESIAN_POINT ( 'NONE',  ( -9.861378660640976790, 146.2806317597711256, 277.1079458220327183 ) ) ;
#10160=ORIENTED_EDGE ( 'NONE', *, *, #9063, .T. ) ;
#10164=CARTESIAN_POINT ( 'NONE',  ( -41.67747345744908216, 165.9786531560170886, 257.1849355913342379 ) ) ;
#10165=CARTESIAN_POINT ( 'NONE',  ( 18.15246772113923512, 187.2525995768337737, 276.0409225219374321 ) ) ;
#10206=EDGE_CURVE ( 'NONE', #15824, #18377, #4336, .T. ) ;
#10217=ADVANCED_FACE ( 'NONE', ( #1023, #22009 ), #8852, .F. ) ;
#10238=STYLED_ITEM ( 'NONE', ( #15432 ), #2374 ) ;
#10249=AXIS2_PLACEMENT_3D ( 'NONE', #6154, #2720, #12827 ) ;
#10259=CARTESIAN_POINT ( 'NONE',  ( -11.00886142849121185, 145.7945275248869734, 276.6464210441237697 ) ) ;
#10289=ORIENTED_EDGE ( 'NONE', *, *, #7129, .F. ) ;
#10295=CARTESIAN_POINT ( 'NONE',  ( -3.188732955586827789, 189.9484169693729996, 274.9698304375367002 ) ) ;
#10304=CARTESIAN_POINT ( 'NONE',  ( 20.28499202003862223, 148.9504299946315768, 278.4103093398852025 ) ) ;
#10317=EDGE_LOOP ( 'NONE', ( #18971, #20750 ) ) ;
#10321=AXIS2_PLACEMENT_3D ( 'NONE', #14995, #21947, #6244 ) ;
#10348=DIRECTION ( 'NONE',  ( 0.01292394549866738782, 0.005513023399720468239, 0.9999012842304692006 ) ) ;
#10351=ADVANCED_FACE ( 'NONE', ( #9068 ), #9314, .T. ) ;
#10368=ORIENTED_EDGE ( 'NONE', *, *, #4507, .T. ) ;
#10377=CARTESIAN_POINT ( 'NONE',  ( -13.08247124652811699, 184.1232080902636596, 278.6476637016128279 ) ) ;
#10393=EDGE_CURVE ( 'NONE', #8741, #5504, #21471, .T. ) ;
#10406=ADVANCED_FACE ( 'NONE', ( #707 ), #19980, .T. ) ;
#10414=ORIENTED_EDGE ( 'NONE', *, *, #8631, .F. ) ;
#10420=CARTESIAN_POINT ( 'NONE',  ( 16.21892470842417922, 145.8010130985019828, 277.5108439706665422 ) ) ;
#10426=B_SPLINE_CURVE_WITH_KNOTS ( 'NONE', 3,
 ( #16154, #3712, #21500, #14310, #10611, #4048, #19773, #10734, #1887, #14430, #48, #2220, #1771, #11073, #8996, #15927, #8751, #15806, #21393, #10953 ),
 .UNSPECIFIED., .F., .F.,
 ( 4, 2, 2, 2, 2, 2, 2, 2, 2, 4 ),
 ( 0.000000000000000000, 0.001733977894910850113, 0.003467955789821700226, 0.005201933684732550772, 0.006935911579643400451, 0.01040386736946519522, 0.01213784526437610735, 0.01300483421183156428, 0.01343832868555929101, 0.01387182315928701948 ),
 .UNSPECIFIED. ) ;
#10427=CYLINDRICAL_SURFACE ( 'NONE', #363, 7.500000000000002665 ) ;
#10430=AXIS2_PLACEMENT_3D ( 'NONE', #1699, #11616, #15609 ) ;
#10439=DIRECTION ( 'NONE',  ( -0.009760756503427833047, 0.9999378516499565217, -0.005387065077611117095 ) ) ;
#10446=AXIS2_PLACEMENT_3D ( 'NONE', #20760, #14127, #10439 ) ;
#10455=ORIENTED_EDGE ( 'NONE', *, *, #16059, .T. ) ;
#10466=ORIENTED_EDGE ( 'NONE', *, *, #16391, .T. ) ;
#10483=DIRECTION ( 'NONE',  ( 0.009760756503427210282, -0.9999378516499566327, 0.005387065077606872227 ) ) ;
#10521=CARTESIAN_POINT ( 'NONE',  ( 51.50086788761742440, 181.5071008296286266, 255.8949677505804061 ) ) ;
#10527=CARTESIAN_POINT ( 'NONE',  ( 3.072605476372664679, 191.4131571344979932, 256.4662960534838589 ) ) ;
#10547=DIRECTION ( 'NONE',  ( 0.9770372205688160339, -0.2127605332646582970, -0.01145535281434409587 ) ) ;
#10558=ADVANCED_FACE ( 'NONE', ( #18938 ), #9386, .F. ) ;
#10568=DIRECTION ( 'NONE',  ( 0.009760756503427813965, -0.9999378516499565217, 0.005387065077607405654 ) ) ;
#10577=VERTEX_POINT ( 'NONE', #17353 ) ;
#10611=CARTESIAN_POINT ( 'NONE',  ( -10.97106015414653157, 147.1489019915714209, 278.5469242478091019 ) ) ;
#10618=DIRECTION ( 'NONE',  ( -0.01297756288283796570, 0.000000000000000000, -0.9999157878849708192 ) ) ;
#10706=DIRECTION ( 'NONE',  ( 0.009760756503428015193, -0.9999378516499566327, 0.005387065077612487526 ) ) ;
#10712=CIRCLE ( 'NONE', #16609, 4.200000000000005507 ) ;
#10734=CARTESIAN_POINT ( 'NONE',  ( -8.648597540386568028, 145.5673199092568950, 277.8375784336965353 ) ) ;
#10765=ORIENTED_EDGE ( 'NONE', *, *, #8103, .T. ) ;
#10772=TOROIDAL_SURFACE ( 'NONE', #6384, 21.67179167071591550, 2.000000000000000000 ) ;
#10779=AXIS2_PLACEMENT_3D ( 'NONE', #4619, #16938, #3015 ) ;
#10786=EDGE_CURVE ( 'NONE', #5976, #17630, #2329, .T. ) ;
#10792=CARTESIAN_POINT ( 'NONE',  ( 51.78636885665599721, 152.2590373701827957, 256.0525387646090394 ) ) ;
#10794=DIRECTION ( 'NONE',  ( 0.9770372205688159228, -0.2127605332646582692, -0.01145535281434409414 ) ) ;
#10796=ADVANCED_FACE ( 'NONE', ( #20044 ), #10772, .T. ) ;
#10816=EDGE_CURVE ( 'NONE', #17630, #20863, #996, .T. ) ;
#10817=CARTESIAN_POINT ( 'NONE',  ( 8.732865712828665750, 190.3249964942741883, 274.4707185275763095 ) ) ;
#10853=EDGE_CURVE ( 'NONE', #10072, #17624, #15928, .T. ) ;
#10855=EDGE_CURVE ( 'NONE', #1725, #13090, #19186, .T. ) ;
#10899=VERTEX_POINT ( 'NONE', #8545 ) ;
#10913=CARTESIAN_POINT ( 'NONE',  ( 20.28256946961299434, 148.9480170188545571, 278.4103539590889227 ) ) ;
#10919=DIRECTION ( 'NONE',  ( 0.01292394549866738782, 0.005513023399720468239, 0.9999012842304692006 ) ) ;
#10953=CARTESIAN_POINT ( 'NONE',  ( -1.632550740186649252, 142.7036636415817838, 274.8672572718561469 ) ) ;
#10960=CARTESIAN_POINT ( 'NONE',  ( 18.16399122330053828, 185.9192657936563648, 277.9565842329805605 ) ) ;
#11035=CIRCLE ( 'NONE', #1147, 26.23296215977917356 ) ;
#11036=DIRECTION ( 'NONE',  ( 0.009760756503427994377, -0.9999378516499565217, 0.005387065077612505741 ) ) ;
#11073=CARTESIAN_POINT ( 'NONE',  ( -2.931228531347772392, 143.0481234405170028, 275.4479384761518190 ) ) ;
#11129=ORIENTED_EDGE ( 'NONE', *, *, #9063, .F. ) ;
#11144=CIRCLE ( 'NONE', #8207, 21.67179167071592261 ) ;
#11160=DIRECTION ( 'NONE',  ( -0.01292394549866738782, -0.005513023399720468239, -0.9999012842304692006 ) ) ;
#11181=VERTEX_POINT ( 'NONE', #7618 ) ;
#11190=EDGE_CURVE ( 'NONE', #13521, #12879, #13692, .T. ) ;
#11234=ORIENTED_EDGE ( 'NONE', *, *, #14367, .T. ) ;
#11264=ORIENTED_EDGE ( 'NONE', *, *, #6679, .T. ) ;
#11282=CARTESIAN_POINT ( 'NONE',  ( 3.072605476372664679, 191.4131571344979932, 256.4662960534838589 ) ) ;
#11294=AXIS2_PLACEMENT_3D ( 'NONE', #3469, #12430, #10483 ) ;
#11296=FACE_OUTER_BOUND ( 'NONE', #9164, .T. ) ;
#11315=CARTESIAN_POINT ( 'NONE',  ( -12.89292530793366431, 186.2522020643850169, 276.6192797974478026 ) ) ;
#11316=VERTEX_POINT ( 'NONE', #3131 ) ;
#11327=VERTEX_POINT ( 'NONE', #12553 ) ;
#11330=CARTESIAN_POINT ( 'NONE',  ( -41.49220022125144425, 173.5884475113861924, 277.1425582878616183 ) ) ;
#11339=CARTESIAN_POINT ( 'NONE',  ( -41.41899454747574083, 166.0889136240115249, 277.1829612759436827 ) ) ;
#11341=AXIS2_PLACEMENT_3D ( 'NONE', #18413, #11400, #2681 ) ;
#11368=UNCERTAINTY_MEASURE_WITH_UNIT (LENGTH_MEASURE( 1.000000000000000082E-05 ), #15216, 'distance_accuracy_value', 'NONE');
#11396=DIRECTION ( 'NONE',  ( 0.9770372205688160339, -0.2127605332646583802, -0.01145535281434409587 ) ) ;
#11400=DIRECTION ( 'NONE',  ( 0.01292394549866738782, 0.005513023399720468239, 0.9999012842304692006 ) ) ;
#11410=CARTESIAN_POINT ( 'NONE',  ( -10.79835136690819120, 187.2594016694268646, 276.3428742396645248 ) ) ;
#11412=DIRECTION ( 'NONE',  ( 0.01292394549866738782, 0.005513023399720468239, 0.9999012842304692006 ) ) ;
#11424=AXIS2_PLACEMENT_3D ( 'NONE', #2439, #2324, #16368 ) ;
#11468=CARTESIAN_POINT ( 'NONE',  ( 48.54425533272844717, 166.9503877551599942, 274.0850249888060830 ) ) ;
#11492=DIRECTION ( 'NONE',  ( 0.01292394549866738782, 0.005513023399720468239, 0.9999012842304692006 ) ) ;
#11506=CARTESIAN_POINT ( 'NONE',  ( -44.86761910970069778, 151.3223208568695952, 257.3069776102678929 ) ) ;
#11554=AXIS2_PLACEMENT_3D ( 'NONE', #20414, #22240, #17014 ) ;
#11565=CARTESIAN_POINT ( 'NONE',  ( -41.52238611146507452, 166.0448094368137504, 269.1837510020998820 ) ) ;
#11582=ORIENTED_EDGE ( 'NONE', *, *, #10855, .F. ) ;
#11598=CARTESIAN_POINT ( 'NONE',  ( 20.04096596137404873, 146.7968166218097110, 276.4111418983213184 ) ) ;
#11616=DIRECTION ( 'NONE',  ( -0.9770372205688155898, 0.2127605332646606839, 0.01145535281434407679 ) ) ;
#11650=CARTESIAN_POINT ( 'NONE',  ( -8.661992976619229623, 145.5753956220379166, 277.8423689545541038 ) ) ;
#11657=CARTESIAN_POINT ( 'NONE',  ( -13.08489379702671052, 184.1207951144569961, 278.6477083146653513 ) ) ;
#11669=CARTESIAN_POINT ( 'NONE',  ( 17.01736581203620702, 186.7717766984534080, 276.5372814302687061 ) ) ;
#11681=CYLINDRICAL_SURFACE ( 'NONE', #11756, 4.200000000000005507 ) ;
#11690=CARTESIAN_POINT ( 'NONE',  ( 17.39319413858549268, 146.5330681163042073, 276.7522768435346165 ) ) ;
#11698=ORIENTED_EDGE ( 'NONE', *, *, #18655, .F. ) ;
#11708=CARTESIAN_POINT ( 'NONE',  ( 48.49599547156344670, 174.4605628858501802, 275.9746324660413279 ) ) ;
#11718=DIRECTION ( 'NONE',  ( -0.004829518060344428765, -0.03945926991566312686, -0.9992095084480668854 ) ) ;
#11756=AXIS2_PLACEMENT_3D ( 'NONE', #11339, #14931, #4545 ) ;
#11762=CARTESIAN_POINT ( 'NONE',  ( -12.87580311257307031, 148.6428581928619792, 277.0426180699594738 ) ) ;
#11766=ADVANCED_FACE ( 'NONE', ( #18944 ), #15645, .F. ) ;
#11773=CARTESIAN_POINT ( 'NONE',  ( -8.806159735684131462, 187.4460332972412857, 276.6223298942460360 ) ) ;
#11789=CARTESIAN_POINT ( 'NONE',  ( 16.54955802965976730, 187.9265162623472349, 275.8329542685239630 ) ) ;
#11804=CARTESIAN_POINT ( 'NONE',  ( -6.157660283484229780, 188.8249578887279085, 276.4363886600518185 ) ) ;
#11833=CIRCLE ( 'NONE', #20972, 1.999999999999997558 ) ;
#11857=CARTESIAN_POINT ( 'NONE',  ( -41.67747345744908216, 165.9786531560170886, 257.1849355913342379 ) ) ;
#11879=VECTOR ( 'NONE', #5485, 999.9999999999998863 ) ;
#11882=CARTESIAN_POINT ( 'NONE',  ( -13.57499642963801634, 147.0376393494719025, 276.9077761425589870 ) ) ;
#11898=VECTOR ( 'NONE', #12493, 1000.000000000000227 ) ;
#11935=DIRECTION ( 'NONE',  ( 0.009760756503427813965, -0.9999378516499565217, 0.005387065077607405654 ) ) ;
#11958=CARTESIAN_POINT ( 'NONE',  ( 9.109368757775373027, 142.0951589094185579, 256.6601876722492648 ) ) ;
#12017=EDGE_LOOP ( 'NONE', ( #9899, #14496, #2936, #11234 ) ) ;
#12069=DIRECTION ( 'NONE',  ( 0.000000000000000000, 0.000000000000000000, 1.000000000000000000 ) ) ;
#12070=( BOUNDED_SURFACE ( )  B_SPLINE_SURFACE ( 3, 2, ( 
 ( #22068, #13828, #6372 ),
 ( #19090, #15339, #1430 ),
 ( #20812, #6582, #10041 ),
 ( #4627, #18977, #13393 ),
 ( #15114, #17273, #16829 ),
 ( #1324, #6482, #5067 ),
 ( #13723, #3235, #11650 ),
 ( #12104, #10153, #13496 ),
 ( #10259, #6698, #8306 ),
 ( #1539, #1211, #18644 ),
 ( #17158, #22292, #8523 ),
 ( #11882, #2909, #20470 ),
 ( #4726, #11762, #22514 ),
 ( #15564, #20706, #18871 ) ),
 .UNSPECIFIED., .F., .F., .T. ) 
 B_SPLINE_SURFACE_WITH_KNOTS ( ( 4, 2, 2, 2, 2, 2, 4 ),
 ( 3, 3 ),
 ( -0.01502904264599872093, -0.01127178198449904113, -0.007514521322999362200, -0.005635890992249522301, -0.003757260661499682835, -0.001878630330749843152, -3.469446951953614189E-18 ),
 ( 0.000000000000000000, 1.000000000000000000 ),
 .UNSPECIFIED. ) 
 GEOMETRIC_REPRESENTATION_ITEM ( )  RATIONAL_B_SPLINE_SURFACE ( (
 ( 1.000000000000000000, 1.000000000000000000, 1.000000000000000000),
 ( 1.000000000000000000, 0.9999832193749498277, 1.000000000000000000),
 ( 1.000000000000000000, 0.9943958665421850363, 1.000000000000000000),
 ( 1.000000000000000000, 0.9719875995013427250, 1.000000000000000000),
 ( 1.000000000000000000, 0.9551974090680757090, 1.000000000000000000),
 ( 1.000000000000000000, 0.9207014414829839399, 1.000000000000000000),
 ( 1.000000000000000000, 0.9076211955268852494, 1.000000000000000000),
 ( 1.000000000000000000, 0.8785736512504284113, 1.000000000000000000),
 ( 1.000000000000000000, 0.8625652577300224610, 1.000000000000000000),
 ( 1.000000000000000000, 0.8274118182163137103, 1.000000000000000000),
 ( 1.000000000000000000, 0.8082693262191131822, 1.000000000000000000),
 ( 1.000000000000000000, 0.7665332262313664380, 1.000000000000000000),
 ( 1.000000000000000000, 0.7439399906329980938, 1.000000000000000000),
 ( 1.000000000000000000, 0.7193398003386509698, 1.000000000000000000) ) ) 
 REPRESENTATION_ITEM ( '' )  SURFACE ( )  );
#12083=EDGE_LOOP ( 'NONE', ( #700, #3965, #2584, #6449 ) ) ;
#12086=CLOSED_SHELL ( 'NONE', ( #20066, #10096, #8630, #5768, #19460, #20853, #8746, #19493, #14881, #8275, #16687, #5798, #21140, #14197, #10351, #21332, #13149, #4437, #19294, #2881, #22513, #4216, #5135, #10406, #10796, #3856, #20312, #10558, #2672, #6415, #14292, #21357, #10217, #3549, #267, #20637, #11766, #8093 ) ) ;
#12091=VECTOR ( 'NONE', #20515, 1000.000000000000114 ) ;
#12104=CARTESIAN_POINT ( 'NONE',  ( -10.48163666083949863, 145.5635402874828230, 276.5713533137832769 ) ) ;
#12118=DIRECTION ( 'NONE',  ( 0.01297756288283796570, 0.000000000000000000, 0.9999157878849708192 ) ) ;
#12129=FACE_OUTER_BOUND ( 'NONE', #144, .T. ) ;
#12141=FACE_BOUND ( 'NONE', #20244, .T. ) ;
#12154=EDGE_LOOP ( 'NONE', ( #20263, #16206, #22415, #2882 ) ) ;
#12162=AXIS2_PLACEMENT_3D ( 'NONE', #4025, #18187, #7711 ) ;
#12201=CARTESIAN_POINT ( 'NONE',  ( 14.28523666940072978, 188.7757037738094255, 275.4832468541452499 ) ) ;
#12225=ORIENTED_EDGE ( 'NONE', *, *, #2, .F. ) ;
#12230=VECTOR ( 'NONE', #19829, 1000.000000000000114 ) ;
#12236=ORIENTED_EDGE ( 'NONE', *, *, #18209, .F. ) ;
#12284=DIRECTION ( 'NONE',  ( 0.009760756503427813965, -0.9999378516499565217, 0.005387065077607405654 ) ) ;
#12286=ORIENTED_EDGE ( 'NONE', *, *, #17071, .T. ) ;
#12335=LINE ( 'NONE', #13626, #16517 ) ;
#12336=ORIENTED_EDGE ( 'NONE', *, *, #6196, .T. ) ;
#12357=DIRECTION ( 'NONE',  ( 0.009760756503428008254, -0.9999378516499564107, 0.005387065077611006073 ) ) ;
#12393=EDGE_LOOP ( 'NONE', ( #18441, #8585, #14601, #5877 ) ) ;
#12406=CARTESIAN_POINT ( 'NONE',  ( 3.316611465012865967, 166.4147053302257007, 256.5999727791399323 ) ) ;
#12413=ORIENTED_EDGE ( 'NONE', *, *, #19667, .F. ) ;
#12430=DIRECTION ( 'NONE',  ( 0.01292394549866738782, 0.005513023399720468239, 0.9999012842304692006 ) ) ;
#12437=CARTESIAN_POINT ( 'NONE',  ( 48.52820596802476416, 171.1607679754053208, 275.9924097807974022 ) ) ;
#12465=DIRECTION ( 'NONE',  ( 0.01292394549866738782, 0.005513023399720468239, 0.9999012842304692006 ) ) ;
#12478=ORIENTED_EDGE ( 'NONE', *, *, #10393, .T. ) ;
#12493=DIRECTION ( 'NONE',  ( -0.02100262710018138690, 0.02843993988601859271, -0.9993748343210220320 ) ) ;
#12506=AXIS2_PLACEMENT_3D ( 'NONE', #6750, #17334, #12284 ) ;
#12525=CARTESIAN_POINT ( 'NONE',  ( 48.26972705805141572, 171.0505075074109129, 255.9943840961880710 ) ) ;
#12531=CARTESIAN_POINT ( 'NONE',  ( 17.15867526775164720, 146.4158769158963196, 277.8065902176103918 ) ) ;
#12534=CARTESIAN_POINT ( 'NONE',  ( -41.52238611146507452, 166.0448094368137504, 269.1837510020998820 ) ) ;
#12547=DIRECTION ( 'NONE',  ( -0.9770372205688160339, 0.2127605332646583802, 0.01145535281434409587 ) ) ;
#12553=CARTESIAN_POINT ( 'NONE',  ( -41.34578887370003031, 158.5893797366368290, 277.2233642640256903 ) ) ;
#12578=DIRECTION ( 'NONE',  ( 0.2317097747526812579, -0.9727820773532223075, 0.002368599673008277024 ) ) ;
#12582=CIRCLE ( 'NONE', #2678, 4.200000000000005507 ) ;
#12596=ORIENTED_EDGE ( 'NONE', *, *, #18209, .T. ) ;
#12613=PLANE ( 'NONE',  #9329 ) ;
#12656=CARTESIAN_POINT ( 'NONE',  ( 16.20940818329404820, 145.7950971976291612, 277.5076651938596797 ) ) ;
#12696=PLANE ( 'NONE',  #20857 ) ;
#12736=FACE_OUTER_BOUND ( 'NONE', #9266, .T. ) ;
#12757=CARTESIAN_POINT ( 'NONE',  ( 3.755496156877637492, 174.6347345924375531, 296.5539275290220189 ) ) ;
#12813=CARTESIAN_POINT ( 'NONE',  ( -14.93612093091044102, 185.1121758471145142, 276.7357782268812798 ) ) ;
#12827=DIRECTION ( 'NONE',  ( 0.2126763768167737323, 0.9770888199431678744, -0.008136134595576589509 ) ) ;
#12839=DIRECTION ( 'NONE',  ( -0.01292394549866738782, -0.005513023399720468239, -0.9999012842304692006 ) ) ;
#12854=ORIENTED_EDGE ( 'NONE', *, *, #17071, .F. ) ;
#12858=CARTESIAN_POINT ( 'NONE',  ( 3.238538336930941508, 174.4142136564487373, 256.5578761598032429 ) ) ;
#12860=EDGE_LOOP ( 'NONE', ( #12854, #16599, #10455, #21243 ) ) ;
#12877=CIRCLE ( 'NONE', #3314, 12.37020706055088759 ) ;
#12879=VERTEX_POINT ( 'NONE', #6884 ) ;
#12900=CARTESIAN_POINT ( 'NONE',  ( -41.56338128877947469, 170.2445484137435585, 269.1611253287739487 ) ) ;
#12946=EDGE_LOOP ( 'NONE', ( #2254, #14153, #15155, #14464 ) ) ;
#12971=VECTOR ( 'NONE', #10794, 1000.000000000000114 ) ;
#13012=CARTESIAN_POINT ( 'NONE',  ( 51.78636885665599010, 152.2590373701828241, 256.0525387646090394 ) ) ;
#13090=VERTEX_POINT ( 'NONE', #10527 ) ;
#13149=ADVANCED_FACE ( 'NONE', ( #12141, #3622, #19127, #20966 ), #8779, .F. ) ;
#13158=CARTESIAN_POINT ( 'NONE',  ( 48.64240681911486774, 159.4614951111008452, 276.0554384422054000 ) ) ;
#13161=DIRECTION ( 'NONE',  ( 0.009760756503427813965, -0.9999378516499565217, 0.005387065077607405654 ) ) ;
#13177=PLANE ( 'NONE',  #2335 ) ;
#13202=TOROIDAL_SURFACE ( 'NONE', #7307, 12.37020706055088759, 2.000000000000000000 ) ;
#13215=AXIS2_PLACEMENT_3D ( 'NONE', #5639, #14748, #10706 ) ;
#13239=ORIENTED_EDGE ( 'NONE', *, *, #20498, .T. ) ;
#13260=CARTESIAN_POINT ( 'NONE',  ( -4.863430190198783087, 189.4649401546927550, 275.2042792935563398 ) ) ;
#13290=AXIS2_PLACEMENT_3D ( 'NONE', #21575, #704, #18175 ) ;
#13296=ORIENTED_EDGE ( 'NONE', *, *, #14162, .F. ) ;
#13298=CARTESIAN_POINT ( 'NONE',  ( 13.25025589056750874, 189.1176631285997303, 275.3030354847988406 ) ) ;
#13323=DIRECTION ( 'NONE',  ( -0.009760756503427893763, 0.9999378516499565217, -0.005387065077610108353 ) ) ;
#13324=DIRECTION ( 'NONE',  ( -0.9770372205688160339, 0.2127605332646584080, 0.01145535281434409587 ) ) ;
#13326=CARTESIAN_POINT ( 'NONE',  ( -41.45998972479013389, 170.2886526009413330, 277.1603356026176925 ) ) ;
#13334=EDGE_LOOP ( 'NONE', ( #21124, #14384, #3371, #1194 ) ) ;
#13382=LINE ( 'NONE', #15555, #19009 ) ;
#13383=FACE_OUTER_BOUND ( 'NONE', #18750, .T. ) ;
#13388=CARTESIAN_POINT ( 'NONE',  ( 8.732865712828665750, 190.3249964942741883, 274.4707185275763095 ) ) ;
#13393=CARTESIAN_POINT ( 'NONE',  ( -5.727992348863838679, 144.0418861141313300, 276.6809104038102305 ) ) ;
#13397=CARTESIAN_POINT ( 'NONE',  ( -41.41899454747574083, 166.0889136240115249, 277.1829612759436827 ) ) ;
#13401=CARTESIAN_POINT ( 'NONE',  ( -14.44752122961171104, 185.3991216854906838, 276.7278808722562076 ) ) ;
#13407=CARTESIAN_POINT ( 'NONE',  ( 9.196690372329060281, 142.8086146031528187, 274.7267082784170498 ) ) ;
#13411=CARTESIAN_POINT ( 'NONE',  ( 19.93803444517712720, 184.4413408268273429, 278.2191123044462984 ) ) ;
#13443=CARTESIAN_POINT ( 'NONE',  ( 17.94009145739756050, 145.7869293583445938, 276.2000847856109544 ) ) ;
#13475=EDGE_LOOP ( 'NONE', ( #12236, #12225 ) ) ;
#13496=CARTESIAN_POINT ( 'NONE',  ( -9.607300630488882831, 146.1747715025532557, 278.1621700325267739 ) ) ;
#13512=CARTESIAN_POINT ( 'NONE',  ( 18.81027419078025176, 185.4549478099342252, 276.6073258177660819 ) ) ;
#13515=DIRECTION ( 'NONE',  ( 0.01292394549866738782, 0.005513023399720468239, 0.9999012842304692006 ) ) ;
#13521=VERTEX_POINT ( 'NONE', #2569 ) ;
#13522=ORIENTED_EDGE ( 'NONE', *, *, #15604, .F. ) ;
#13535=CARTESIAN_POINT ( 'NONE',  ( 14.49661276311460334, 144.7736480898878426, 276.2294396764298767 ) ) ;
#13566=( LENGTH_UNIT ( ) NAMED_UNIT ( * ) SI_UNIT ( .MILLI., .METRE. ) );
#13611=DIRECTION ( 'NONE',  ( -0.009760756503428008254, 0.9999378516499565217, -0.005387065077611300108 ) ) ;
#13614=CARTESIAN_POINT ( 'NONE',  ( -11.79420393680612023, 185.2698227558952624, 278.4462014808021308 ) ) ;
#13626=CARTESIAN_POINT ( 'NONE',  ( -41.34578887370003031, 158.5893797366368290, 277.2233642640256903 ) ) ;
#13642=CARTESIAN_POINT ( 'NONE',  ( -2.096375399687082197, 190.2200455327031534, 274.6112675210154634 ) ) ;
#13648=AXIS2_PLACEMENT_3D ( 'NONE', #3177, #15392, #13877 ) ;
#13650=CARTESIAN_POINT ( 'NONE',  ( 17.63467579678667008, 146.7507910439422858, 277.9425923883162568 ) ) ;
#13660=CIRCLE ( 'NONE', #13290, 14.36898871458908111 ) ;
#13692=B_SPLINE_CURVE_WITH_KNOTS ( 'NONE', 3,
 ( #3939, #9454, #7740, #21504, #10960, #14779, #17986, #21730, #517, #18104, #7517, #5770, #2347, #1535, #22288, #21945, #6242, #17270, #15232, #13388 ),
 .UNSPECIFIED., .F., .F.,
 ( 4, 2, 2, 2, 2, 2, 2, 2, 2, 4 ),
 ( 0.000000000000000000, 0.001733977894910813684, 0.003467955789821627367, 0.005201933684732441485, 0.006935911579643254735, 0.01040386736946483266, 0.01213784526437566152, 0.01300483421183110805, 0.01343832868555880182, 0.01387182315928649386 ),
 .UNSPECIFIED. ) ;
#13723=CARTESIAN_POINT ( 'NONE',  ( -9.411766176742821344, 145.1181305486205702, 276.4045370640140504 ) ) ;
#13744=CARTESIAN_POINT ( 'NONE',  ( 3.316624388958365088, 166.4147108432491109, 256.6009726804241495 ) ) ;
#13824=CARTESIAN_POINT ( 'NONE',  ( -8.560375375394391639, 187.5535857524832295, 277.4257007466420646 ) ) ;
#13828=CARTESIAN_POINT ( 'NONE',  ( -1.632550740186646143, 142.7036636415817838, 274.8672572718561469 ) ) ;
#13877=DIRECTION ( 'NONE',  ( 0.6916826046072646061, 0.7220860138273254014, -0.01292142092318427499 ) ) ;
#13911=CARTESIAN_POINT ( 'NONE',  ( 9.858392366551100849, 190.0737637416658288, 274.6814703483424864 ) ) ;
#13927=EDGE_LOOP ( 'NONE', ( #20040, #266, #8504, #14990 ) ) ;
#13952=CARTESIAN_POINT ( 'NONE',  ( -41.52238611146507452, 166.0448094368137504, 269.1837510020998820 ) ) ;
#13978=CARTESIAN_POINT ( 'NONE',  ( 18.54481925875508708, 147.4389108747255364, 278.1650990181268526 ) ) ;
#13986=DIRECTION ( 'NONE',  ( -0.01292394549866738782, -0.005513023399720468239, -0.9999012842304692006 ) ) ;
#13990=EDGE_LOOP ( 'NONE', ( #14549, #6793, #10289, #17977 ) ) ;
#14006=DIRECTION ( 'NONE',  ( -0.2311175842251773915, 0.9723818865373500264, 0.03252889478574687993 ) ) ;
#14019=EDGE_LOOP ( 'NONE', ( #16163, #12286 ) ) ;
#14022=ORIENTED_EDGE ( 'NONE', *, *, #1226, .T. ) ;
#14057=CARTESIAN_POINT ( 'NONE',  ( 20.02943147455619410, 184.4085440663593545, 276.4201140974324744 ) ) ;
#14064=VECTOR ( 'NONE', #13324, 999.9999999999998863 ) ;
#14070=ORIENTED_EDGE ( 'NONE', *, *, #2338, .T. ) ;
#14113=FACE_BOUND ( 'NONE', #17339, .T. ) ;
#14121=EDGE_CURVE ( 'NONE', #12879, #10577, #895, .T. ) ;
#14127=DIRECTION ( 'NONE',  ( -0.01292394549866738782, -0.005513023399720468239, -0.9999012842304692006 ) ) ;
#14146=VERTEX_POINT ( 'NONE', #16889 ) ;
#14153=ORIENTED_EDGE ( 'NONE', *, *, #18593, .T. ) ;
#14162=EDGE_CURVE ( 'NONE', #345, #2627, #22512, .T. ) ;
#14170=CYLINDRICAL_SURFACE ( 'NONE', #11294, 4.200000000000005507 ) ;
#14186=DIRECTION ( 'NONE',  ( -0.01292394549866738782, -0.005513023399720468239, -0.9999012842304692006 ) ) ;
#14197=ADVANCED_FACE ( 'NONE', ( #19034 ), #18523, .T. ) ;
#14223=CARTESIAN_POINT ( 'NONE',  ( 3.316624388958365088, 166.4147108432491109, 256.6009726804241495 ) ) ;
#14229=EDGE_LOOP ( 'NONE', ( #2419, #17072, #485, #9125 ) ) ;
#14260=CARTESIAN_POINT ( 'NONE',  ( 11.78612559536878734, 143.6154693132956766, 275.8089238432258412 ) ) ;
#14275=LINE ( 'NONE', #1643, #19210 ) ;
#14282=CARTESIAN_POINT ( 'NONE',  ( -2.476119979858705467, 190.7342627770796355, 256.5417576885990343 ) ) ;
#14290=( GEOMETRIC_REPRESENTATION_CONTEXT ( 3 ) GLOBAL_UNCERTAINTY_ASSIGNED_CONTEXT ( ( #11368 ) ) GLOBAL_UNIT_ASSIGNED_CONTEXT ( ( #15216, #3000, #6224 ) ) REPRESENTATION_CONTEXT ( 'NONE', 'WORKASPACE' ) );
#14292=ADVANCED_FACE ( 'NONE', ( #3535 ), #7531, .T. ) ;
#14310=CARTESIAN_POINT ( 'NONE',  ( -11.41931823208222774, 147.4996510494855215, 278.6483820114981995 ) ) ;
#14344=CARTESIAN_POINT ( 'NONE',  ( -45.15312007873931321, 180.5703843163154545, 257.1494065962392597 ) ) ;
#14364=CIRCLE ( 'NONE', #389, 12.37020706055088759 ) ;
#14367=EDGE_CURVE ( 'NONE', #15447, #8963, #22142, .T. ) ;
#14384=ORIENTED_EDGE ( 'NONE', *, *, #963, .T. ) ;
#14386=CARTESIAN_POINT ( 'NONE',  ( 13.29718515720261607, 144.2203306461185264, 276.4281824851719875 ) ) ;
#14391=AXIS2_PLACEMENT_3D ( 'NONE', #3240, #6705, #13611 ) ;
#14404=ORIENTED_EDGE ( 'NONE', *, *, #6692, .T. ) ;
#14430=CARTESIAN_POINT ( 'NONE',  ( -6.705340559502253051, 144.4905701593873459, 277.0953757322560591 ) ) ;
#14464=ORIENTED_EDGE ( 'NONE', *, *, #4591, .T. ) ;
#14490=DIRECTION ( 'NONE',  ( 0.009760756503428048153, -0.9999378516499565217, 0.005387065077612505741 ) ) ;
#14496=ORIENTED_EDGE ( 'NONE', *, *, #19194, .T. ) ;
#14497=CARTESIAN_POINT ( 'NONE',  ( -4.153117824915283585, 189.6079574532614060, 275.5417844139159911 ) ) ;
#14501=CARTESIAN_POINT ( 'NONE',  ( 18.53667494532311721, 147.4324440254954993, 278.1633530095816127 ) ) ;
#14502=LINE ( 'NONE', #2642, #6593 ) ;
#14522=CARTESIAN_POINT ( 'NONE',  ( -2.752290252500367629, 142.9573650401683267, 275.1042456662929681 ) ) ;
#14549=ORIENTED_EDGE ( 'NONE', *, *, #4177, .T. ) ;
#14573=LINE ( 'NONE', #2383, #22491 ) ;
#14601=ORIENTED_EDGE ( 'NONE', *, *, #18755, .T. ) ;
#14622=DIRECTION ( 'NONE',  ( -0.9770372205688159228, 0.2127605332646583802, 0.01145535281434409414 ) ) ;
#14672=AXIS2_PLACEMENT_3D ( 'NONE', #12534, #10919, #16230 ) ;
#14694=CARTESIAN_POINT ( 'NONE',  ( 3.394710440985788669, 158.4152080300494561, 256.6440692010450562 ) ) ;
#14722=CARTESIAN_POINT ( 'NONE',  ( -41.41899454747574083, 166.0889136240115249, 277.1829612759436827 ) ) ;
#14748=DIRECTION ( 'NONE',  ( -0.01292394549866738782, -0.005513023399720468239, -0.9999012842304692006 ) ) ;
#14753=CARTESIAN_POINT ( 'NONE',  ( -12.50473920891009882, 146.4814768226545141, 276.8334956993934384 ) ) ;
#14760=EDGE_LOOP ( 'NONE', ( #10160, #8284, #16424, #2518 ) ) ;
#14767=DIRECTION ( 'NONE',  ( -0.005493774068846058074, 0.02859024303483492097, -0.9995761183870338629 ) ) ;
#14779=CARTESIAN_POINT ( 'NONE',  ( 17.24533165808599477, 186.5834384566230995, 277.7277893435518763 ) ) ;
#14783=CARTESIAN_POINT ( 'NONE',  ( 22.08632752877390359, 147.9377667753725802, 276.4622185031857384 ) ) ;
#14784=VERTEX_POINT ( 'NONE', #11708 ) ;
#14867=CARTESIAN_POINT ( 'NONE',  ( -3.863860647413861926, 143.2476736384784033, 275.3398486090524102 ) ) ;
#14881=ADVANCED_FACE ( 'NONE', ( #19382 ), #9031, .T. ) ;
#14890=CARTESIAN_POINT ( 'NONE',  ( 3.600049111542418689, 166.5356125545590373, 278.5290088303507332 ) ) ;
#14920=CARTESIAN_POINT ( 'NONE',  ( 9.796239224404398982, 190.0809038477337651, 274.9155399994040181 ) ) ;
#14931=DIRECTION ( 'NONE',  ( 0.01292394549866738782, 0.005513023399720468239, 0.9999012842304692006 ) ) ;
#14938=DIRECTION ( 'NONE',  ( 0.009760756503427813965, -0.9999378516499565217, 0.005387065077611106687 ) ) ;
#14973=DIRECTION ( 'NONE',  ( 0.009760756503427210282, -0.9999378516499566327, 0.005387065077606872227 ) ) ;
#14977=SURFACE_SIDE_STYLE ('',( #7947 ) ) ;
#14990=ORIENTED_EDGE ( 'NONE', *, *, #8209, .T. ) ;
#14995=CARTESIAN_POINT ( 'NONE',  ( 51.78636885665599010, 152.2590373701828241, 256.0525387646090394 ) ) ;
#14996=VECTOR ( 'NONE', #11396, 999.9999999999998863 ) ;
#15000=DIRECTION ( 'NONE',  ( 0.01292394549866738782, 0.005513023399720468239, 0.9999012842304692006 ) ) ;
#15019=CARTESIAN_POINT ( 'NONE',  ( 10.83543253063041689, 189.7684987719255503, 275.3551034107306350 ) ) ;
#15099=ORIENTED_EDGE ( 'NONE', *, *, #4460, .F. ) ;
#15114=CARTESIAN_POINT ( 'NONE',  ( -7.227204710067946181, 144.2888362340090396, 276.0193614813773593 ) ) ;
#15123=CARTESIAN_POINT ( 'NONE',  ( -6.558142562982950174, 188.9283497255633506, 275.5585268130429881 ) ) ;
#15127=DIRECTION ( 'NONE',  ( -0.009760756503427833047, 0.9999378516499565217, -0.005387065077611117095 ) ) ;
#15155=ORIENTED_EDGE ( 'NONE', *, *, #584, .T. ) ;
#15161=VERTEX_POINT ( 'NONE', #20507 ) ;
#15169=AXIS2_PLACEMENT_3D ( 'NONE', #12406, #21337, #14490 ) ;
#15194=AXIS2_PLACEMENT_3D ( 'NONE', #3406, #15831, #7190 ) ;
#15216=( LENGTH_UNIT ( ) NAMED_UNIT ( * ) SI_UNIT ( .MILLI., .METRE. ) );
#15232=CARTESIAN_POINT ( 'NONE',  ( 8.863278656984560300, 190.2950607885061061, 274.5252716332005321 ) ) ;
#15244=CARTESIAN_POINT ( 'NONE',  ( -9.798971742014797925, 187.6828575582066492, 276.1705134504438774 ) ) ;
#15254=CARTESIAN_POINT ( 'NONE',  ( 14.08299609623372639, 188.4741397916250207, 275.9973987394899950 ) ) ;
#15269=CARTESIAN_POINT ( 'NONE',  ( -4.352520608367785648, 189.6274523698270684, 275.0976271054587414 ) ) ;
#15277=CARTESIAN_POINT ( 'NONE',  ( 19.98859775871076039, 148.6042059346136455, 276.7049348957753523 ) ) ;
#15301=CARTESIAN_POINT ( 'NONE',  ( 3.575103298931712636, 166.5249713112435188, 276.5989983650335375 ) ) ;
#15334=ORIENTED_EDGE ( 'NONE', *, *, #2216, .T. ) ;
#15339=CARTESIAN_POINT ( 'NONE',  ( -2.729922624342409065, 142.9577372919816582, 275.2229497859695471 ) ) ;
#15345=CARTESIAN_POINT ( 'NONE',  ( -13.95214564498276211, 185.6760471167460480, 276.6996455583582701 ) ) ;
#15359=DIRECTION ( 'NONE',  ( 0.01292394549866738782, 0.005513023399720468239, 0.9999012842304692006 ) ) ;
#15370=EDGE_LOOP ( 'NONE', ( #18990, #16476, #35, #21551 ) ) ;
#15376=ORIENTED_EDGE ( 'NONE', *, *, #9653, .T. ) ;
#15382=CARTESIAN_POINT ( 'NONE',  ( 10.34070483759711401, 143.0898343825529935, 274.9390076312643032 ) ) ;
#15392=DIRECTION ( 'NONE',  ( 0.7220859686467110405, -0.6917813203664554544, -0.005518937903674935030 ) ) ;
#15400=VECTOR ( 'NONE', #3522, 999.9999999999998863 ) ;
#15422=CIRCLE ( 'NONE', #13215, 8.000000000000012434 ) ;
#15428=FACE_OUTER_BOUND ( 'NONE', #8922, .T. ) ;
#15432=PRESENTATION_STYLE_ASSIGNMENT (( #8388 ) ) ;
#15447=VERTEX_POINT ( 'NONE', #2242 ) ;
#15494=PRODUCT_DEFINITION_CONTEXT ( 'detailed design', #752, 'design' ) ;
#15496=DIRECTION ( 'NONE',  ( 0.009760756503427813965, -0.9999378516499565217, 0.005387065077607405654 ) ) ;
#15499=CARTESIAN_POINT ( 'NONE',  ( -45.15312007873932032, 180.5703843163154261, 257.1494065962392597 ) ) ;
#15508=CARTESIAN_POINT ( 'NONE',  ( 22.08632752877390359, 147.9377667753725802, 276.4622185031857384 ) ) ;
#15532=AXIS2_PLACEMENT_3D ( 'NONE', #11468, #18353, #13323 ) ;
#15539=CARTESIAN_POINT ( 'NONE',  ( -13.57324918674249936, 183.7437101232661973, 276.7257079361987167 ) ) ;
#15545=AXIS2_PLACEMENT_3D ( 'NONE', #10164, #15359, #18994 ) ;
#15548=EDGE_CURVE ( 'NONE', #10577, #6314, #11035, .T. ) ;
#15553=FACE_OUTER_BOUND ( 'NONE', #14229, .T. ) ;
#15555=CARTESIAN_POINT ( 'NONE',  ( 3.560643301544068162, 141.4162645520002002, 256.7356493073644401 ) ) ;
#15564=CARTESIAN_POINT ( 'NONE',  ( -14.56978029430814203, 147.5825162344054888, 276.9379655111616785 ) ) ;
#15601=CIRCLE ( 'NONE', #9734, 4.200000000000005507 ) ;
#15603=CARTESIAN_POINT ( 'NONE',  ( 15.95581455245526392, 145.6036739495936274, 276.5329765736894387 ) ) ;
#15604=EDGE_CURVE ( 'NONE', #19271, #13521, #9183, .T. ) ;
#15609=DIRECTION ( 'NONE',  ( -0.2126763768167770630, -0.9770888199431673193, 0.008136134595576584305 ) ) ;
#15645=CYLINDRICAL_SURFACE ( 'NONE', #2737, 7.500000000000002665 ) ;
#15659=VERTEX_POINT ( 'NONE', #19323 ) ;
#15668=VERTEX_POINT ( 'NONE', #2443 ) ;
#15692=ORIENTED_EDGE ( 'NONE', *, *, #18593, .F. ) ;
#15705=CARTESIAN_POINT ( 'NONE',  ( -2.096375399687082197, 190.2200455327031534, 274.6112675210154634 ) ) ;
#15716=CARTESIAN_POINT ( 'NONE',  ( 19.85977264408844079, 148.5551973574642943, 278.3773732832850101 ) ) ;
#15746=CIRCLE ( 'NONE', #11341, 24.99999999999998224 ) ;
#15764=EDGE_CURVE ( 'NONE', #6123, #5251, #17643, .T. ) ;
#15766=AXIS2_PLACEMENT_3D ( 'NONE', #22348, #1598, #22464 ) ;
#15790=CARTESIAN_POINT ( 'NONE',  ( 48.31072223536580879, 166.8507685304811048, 256.0170097695140043 ) ) ;
#15806=CARTESIAN_POINT ( 'NONE',  ( -1.893392603924682671, 142.7666083241327328, 274.9837640348721379 ) ) ;
#15824=VERTEX_POINT ( 'NONE', #1273 ) ;
#15831=DIRECTION ( 'NONE',  ( 0.01292394549866738608, 0.005513023399720468239, 0.9999012842304692006 ) ) ;
#15835=AXIS2_PLACEMENT_3D ( 'NONE', #16392, #2702, #6377 ) ;
#15858=CIRCLE ( 'NONE', #8129, 2.000000000000008438 ) ;
#15902=CARTESIAN_POINT ( 'NONE',  ( 13.87343267002348846, 188.5565630873763325, 276.5910899882047147 ) ) ;
#15905=EDGE_CURVE ( 'NONE', #5251, #14784, #22321, .T. ) ;
#15913=DIRECTION ( 'NONE',  ( 0.009760756503427210282, -0.9999378516499566327, 0.005387065077606872227 ) ) ;
#15925=CARTESIAN_POINT ( 'NONE',  ( 3.560643301544068162, 141.4162645520002002, 256.7356493073644401 ) ) ;
#15927=CARTESIAN_POINT ( 'NONE',  ( -2.283878053185306456, 142.8671684950954841, 275.1583867193013475 ) ) ;
#15928=CIRCLE ( 'NONE', #19204, 7.999999999999985789 ) ;
#15968=AXIS2_PLACEMENT_3D ( 'NONE', #18555, #2366, #15127 ) ;
#15974=EDGE_CURVE ( 'NONE', #14784, #16406, #19822, .T. ) ;
#16023=DIRECTION ( 'NONE',  ( -0.02100262710018139731, 0.02843993988601858577, -0.9993748343210220320 ) ) ;
#16025=ORIENTED_EDGE ( 'NONE', *, *, #406, .T. ) ;
#16038=ORIENTED_EDGE ( 'NONE', *, *, #21695, .T. ) ;
#16059=EDGE_CURVE ( 'NONE', #20863, #11327, #414, .T. ) ;
#16091=FACE_OUTER_BOUND ( 'NONE', #3308, .T. ) ;
#16105=CARTESIAN_POINT ( 'NONE',  ( 10.24508981178217937, 143.0941829715302731, 275.1657397502952449 ) ) ;
#16154=CARTESIAN_POINT ( 'NONE',  ( -13.16231198119108114, 149.0364497547966209, 278.8421488773936403 ) ) ;
#16163=ORIENTED_EDGE ( 'NONE', *, *, #10786, .T. ) ;
#16186=EDGE_LOOP ( 'NONE', ( #7903, #16581, #6655, #12596 ) ) ;
#16206=ORIENTED_EDGE ( 'NONE', *, *, #21003, .T. ) ;
#16228=DIRECTION ( 'NONE',  ( -0.02033837109167978621, -0.03960957306447945164, -0.9990082243820552765 ) ) ;
#16230=DIRECTION ( 'NONE',  ( 0.009760756503427210282, -0.9999378516499566327, 0.005387065077606872227 ) ) ;
#16254=DIRECTION ( 'NONE',  ( -0.01325671806966821978, 0.02938766274154132677, -0.9994801772444567023 ) ) ;
#16293=CARTESIAN_POINT ( 'NONE',  ( -1.208359178344593055, 144.6562660457661025, 274.7812028121480807 ) ) ;
#16321=DIRECTION ( 'NONE',  ( 0.009760756503427813965, -0.9999378516499565217, 0.005387065077607405654 ) ) ;
#16359=CARTESIAN_POINT ( 'NONE',  ( 3.316624388958365088, 166.4147108432491109, 256.6009726804241495 ) ) ;
#16367=CARTESIAN_POINT ( 'NONE',  ( 48.35171741268020185, 162.6510295535512682, 256.0396354428399945 ) ) ;
#16368=DIRECTION ( 'NONE',  ( 0.009760756503427210282, -0.9999378516499566327, 0.005387065077606872227 ) ) ;
#16381=CARTESIAN_POINT ( 'NONE',  ( -13.16231198119108114, 149.0364497547966209, 278.8421488773936403 ) ) ;
#16390=CARTESIAN_POINT ( 'NONE',  ( -14.91027303991310404, 185.1232018939139436, 278.7355807953422300 ) ) ;
#16391=EDGE_CURVE ( 'NONE', #20552, #10899, #20224, .T. ) ;
#16392=CARTESIAN_POINT ( 'NONE',  ( 3.316624388958365088, 166.4147108432491109, 256.6009726804241495 ) ) ;
#16405=DIRECTION ( 'NONE',  ( 0.009760756503428008254, -0.9999378516499564107, 0.005387065077611006073 ) ) ;
#16406=VERTEX_POINT ( 'NONE', #5075 ) ;
#16419=EDGE_LOOP ( 'NONE', ( #3749, #16673, #4677, #13522 ) ) ;
#16424=ORIENTED_EDGE ( 'NONE', *, *, #15548, .T. ) ;
#16476=ORIENTED_EDGE ( 'NONE', *, *, #641, .F. ) ;
#16494=CARTESIAN_POINT ( 'NONE',  ( -41.63647828013468910, 161.7789141790872804, 257.2075612646602281 ) ) ;
#16517=VECTOR ( 'NONE', #8225, 999.9999999999998863 ) ;
#16544=ORIENTED_EDGE ( 'NONE', *, *, #21272, .T. ) ;
#16547=ORIENTED_EDGE ( 'NONE', *, *, #6196, .F. ) ;
#16575=TOROIDAL_SURFACE ( 'NONE', #5902, 26.23296215977915935, 2.000000000000000000 ) ;
#16581=ORIENTED_EDGE ( 'NONE', *, *, #9630, .F. ) ;
#16599=ORIENTED_EDGE ( 'NONE', *, *, #10816, .T. ) ;
#16609=AXIS2_PLACEMENT_3D ( 'NONE', #5493, #19174, #3448 ) ;
#16673=ORIENTED_EDGE ( 'NONE', *, *, #15548, .F. ) ;
#16687=ADVANCED_FACE ( 'NONE', ( #18525 ), #22168, .T. ) ;
#16689=DIRECTION ( 'NONE',  ( 0.9726991065672921932, 0.2316562896908778701, -0.01384960395994898341 ) ) ;
#16693=CARTESIAN_POINT ( 'NONE',  ( -41.37799937016134777, 161.8891746470816884, 277.2055869492696161 ) ) ;
#16706=AXIS2_PLACEMENT_3D ( 'NONE', #6934, #9947, #18999 ) ;
#16716=VERTEX_POINT ( 'NONE', #9898 ) ;
#16727=FACE_OUTER_BOUND ( 'NONE', #12946, .T. ) ;
#16754=ORIENTED_EDGE ( 'NONE', *, *, #5040, .F. ) ;
#16765=CARTESIAN_POINT ( 'NONE',  ( 22.08632752877390715, 147.9377667753725802, 276.4622185031857384 ) ) ;
#16799=CARTESIAN_POINT ( 'NONE',  ( -10.39470828226744636, 145.5140731825025284, 276.5683172678064352 ) ) ;
#16829=CARTESIAN_POINT ( 'NONE',  ( -6.716850738106426633, 144.4960990889537413, 277.1001543104694633 ) ) ;
#16840=VECTOR ( 'NONE', #22155, 1000.000000000000114 ) ;
#16870=CARTESIAN_POINT ( 'NONE',  ( 21.59772782749408648, 147.6508209369730196, 276.4701158578107538 ) ) ;
#16872=EDGE_CURVE ( 'NONE', #18377, #8063, #1891, .T. ) ;
#16885=CARTESIAN_POINT ( 'NONE',  ( 9.196690372329049623, 142.8086146031528187, 274.7267082784170498 ) ) ;
#16889=CARTESIAN_POINT ( 'NONE',  ( 9.109368757775365921, 142.0951589094185579, 256.6601876722492648 ) ) ;
#16906=CARTESIAN_POINT ( 'NONE',  ( 51.50086788761742440, 181.5071008296286266, 255.8949677505804061 ) ) ;
#16920=VERTEX_POINT ( 'NONE', #12525 ) ;
#16938=DIRECTION ( 'NONE',  ( 0.01292394549866738782, 0.005513023399720468239, 0.9999012842304692006 ) ) ;
#16939=EDGE_LOOP ( 'NONE', ( #22388, #21414, #22496, #17911 ) ) ;
#16951=CIRCLE ( 'NONE', #19846, 23.67057332475409126 ) ;
#16955=CARTESIAN_POINT ( 'NONE',  ( -11.35185528768898600, 185.6292709456122907, 278.3409550216183561 ) ) ;
#16989=CARTESIAN_POINT ( 'NONE',  ( -3.234480676511187980, 189.9413464613920723, 274.8561509274957757 ) ) ;
#16997=CARTESIAN_POINT ( 'NONE',  ( 14.77414660359919374, 144.4974462979978398, 275.7313215082337479 ) ) ;
#17006=DIRECTION ( 'NONE',  ( -0.7220859686467110405, 0.6917813203664554544, 0.005518937903674876050 ) ) ;
#17014=DIRECTION ( 'NONE',  ( -0.2317097747526779827, 0.9727820773532231957, -0.002368599673008279193 ) ) ;
#17024=CIRCLE ( 'NONE', #6388, 4.200000000000005507 ) ;
#17056=ORIENTED_EDGE ( 'NONE', *, *, #10393, .F. ) ;
#17069=CARTESIAN_POINT ( 'NONE',  ( -12.83272386646220475, 184.4481542101678713, 276.9315297105506488 ) ) ;
#17071=EDGE_CURVE ( 'NONE', #17630, #5976, #9622, .T. ) ;
#17072=ORIENTED_EDGE ( 'NONE', *, *, #9799, .F. ) ;
#17075=ORIENTED_EDGE ( 'NONE', *, *, #6294, .T. ) ;
#17092=ORIENTED_EDGE ( 'NONE', *, *, #10853, .F. ) ;
#17101=CARTESIAN_POINT ( 'NONE',  ( 19.58193934041550932, 146.5773600902072360, 276.3640708165659703 ) ) ;
#17158=CARTESIAN_POINT ( 'NONE',  ( -12.56198361051020918, 146.5221865386392324, 276.8288772454161517 ) ) ;
#17184=ORIENTED_EDGE ( 'NONE', *, *, #4177, .F. ) ;
#17201=FACE_OUTER_BOUND ( 'NONE', #21555, .T. ) ;
#17246=CARTESIAN_POINT ( 'NONE',  ( -41.48139093415068146, 161.8450704598839138, 269.2063766754258722 ) ) ;
#17264=EDGE_LOOP ( 'NONE', ( #5149, #9536 ) ) ;
#17270=CARTESIAN_POINT ( 'NONE',  ( 8.996640567037356817, 190.2633029501699014, 274.5811317046487829 ) ) ;
#17273=CARTESIAN_POINT ( 'NONE',  ( -6.941700055406210268, 144.5720018159295819, 276.5112050013826206 ) ) ;
#17334=DIRECTION ( 'NONE',  ( 0.01292394549866738782, 0.005513023399720468239, 0.9999012842304692006 ) ) ;
#17339=EDGE_LOOP ( 'NONE', ( #21269, #17484 ) ) ;
#17342=CYLINDRICAL_SURFACE ( 'NONE', #2903, 2.000000000000008438 ) ;
#17353=CARTESIAN_POINT ( 'NONE',  ( 21.71998689217155132, 185.4674263880815204, 276.2600312189053966 ) ) ;
#17377=EDGE_LOOP ( 'NONE', ( #4210, #22575, #14022, #7981 ) ) ;
#17390=CARTESIAN_POINT ( 'NONE',  ( -9.975585911415770113, 186.6480926472742112, 277.9354835072872447 ) ) ;
#17392=CIRCLE ( 'NONE', #8555, 26.23296215977917356 ) ;
#17420=FACE_OUTER_BOUND ( 'NONE', #12154, .T. ) ;
#17429=CARTESIAN_POINT ( 'NONE',  ( -4.162724741132324269, 189.6234579029260487, 275.5491270811696154 ) ) ;
#17437=CARTESIAN_POINT ( 'NONE',  ( 16.93665130137262764, 145.3617413512261010, 276.0582899410866276 ) ) ;
#17484=ORIENTED_EDGE ( 'NONE', *, *, #2623, .F. ) ;
#17496=CARTESIAN_POINT ( 'NONE',  ( 52.66525871368118317, 166.9576235287527481, 267.9613219752613418 ) ) ;
#17514=ORIENTED_EDGE ( 'NONE', *, *, #2926, .T. ) ;
#17540=EDGE_LOOP ( 'NONE', ( #11582, #20983, #9596, #18937, #6405, #21873, #2978, #2890, #7066, #6229 ) ) ;
#17610=ORIENTED_EDGE ( 'NONE', *, *, #16872, .F. ) ;
#17624=VERTEX_POINT ( 'NONE', #18103 ) ;
#17630=VERTEX_POINT ( 'NONE', #4387 ) ;
#17631=CONICAL_SURFACE ( 'NONE', #4030, 15.00000000000000533, 0.03490658503988662564 ) ;
#17643=CIRCLE ( 'NONE', #12506, 7.500000000000002665 ) ;
#17669=CYLINDRICAL_SURFACE ( 'NONE', #4131, 4.200000000000005507 ) ;
#17698=LINE ( 'NONE', #10792, #12230 ) ;
#17700=LINE ( 'NONE', #9160, #12971 ) ;
#17705=VERTEX_POINT ( 'NONE', #21610 ) ;
#17834=VERTEX_POINT ( 'NONE', #20582 ) ;
#17836=CARTESIAN_POINT ( 'NONE',  ( 9.722607335555387920, 142.9425743169972520, 274.9463719921606071 ) ) ;
#17869=VERTEX_POINT ( 'NONE', #20674 ) ;
#17891=VECTOR ( 'NONE', #11718, 1000.000000000000114 ) ;
#17902=DIRECTION ( 'NONE',  ( -0.009760756503428008254, 0.9999378516499564107, -0.005387065077611006073 ) ) ;
#17911=ORIENTED_EDGE ( 'NONE', *, *, #20592, .F. ) ;
#17936=CARTESIAN_POINT ( 'NONE',  ( 20.70083805927512088, 149.3646325075532957, 278.4026507072620120 ) ) ;
#17977=ORIENTED_EDGE ( 'NONE', *, *, #19452, .F. ) ;
#17986=CARTESIAN_POINT ( 'NONE',  ( 16.77746333736591566, 186.8979171237260459, 277.5925732922278257 ) ) ;
#18055=AXIS2_PLACEMENT_3D ( 'NONE', #1060, #6673, #20559 ) ;
#18075=CARTESIAN_POINT ( 'NONE',  ( -13.54442673061105573, 147.0068218323744134, 276.9278867193614246 ) ) ;
#18103=CARTESIAN_POINT ( 'NONE',  ( 3.911668260932484209, 158.6357289660382719, 296.6401205702638322 ) ) ;
#18104=CARTESIAN_POINT ( 'NONE',  ( 13.86180204460999299, 188.5620406374387414, 276.5865498250307155 ) ) ;
#18175=DIRECTION ( 'NONE',  ( -0.009760756503427874681, 0.9999378516499565217, -0.005387065077610097945 ) ) ;
#18187=DIRECTION ( 'NONE',  ( 0.01292394549866738608, 0.005513023399720468239, 0.9999012842304692006 ) ) ;
#18209=EDGE_CURVE ( 'NONE', #11181, #15659, #10712, .T. ) ;
#18244=CARTESIAN_POINT ( 'NONE',  ( 48.56920114533915722, 166.9610289984755127, 276.0150354541233924 ) ) ;
#18251=CARTESIAN_POINT ( 'NONE',  ( 51.50086788761742440, 181.5071008296286266, 255.8949677505804061 ) ) ;
#18282=CARTESIAN_POINT ( 'NONE',  ( -1.634140231236729024, 188.2752817596284842, 274.5462097314439234 ) ) ;
#18300=CARTESIAN_POINT ( 'NONE',  ( -7.586966048391873940, 188.5645970664055255, 275.7666243300806173 ) ) ;
#18326=FACE_OUTER_BOUND ( 'NONE', #849, .T. ) ;
#18329=CARTESIAN_POINT ( 'NONE',  ( 3.807734317907725430, 166.6242057324384689, 294.5972214811819754 ) ) ;
#18337=ORIENTED_EDGE ( 'NONE', *, *, #15905, .F. ) ;
#18339=FACE_OUTER_BOUND ( 'NONE', #13334, .T. ) ;
#18353=DIRECTION ( 'NONE',  ( -0.01292394549866738782, -0.005513023399720468239, -0.9999012842304692006 ) ) ;
#18372=( BOUNDED_SURFACE ( )  B_SPLINE_SURFACE ( 3, 2, ( 
 ( #1514, #15539, #22488 ),
 ( #13401, #20476, #11657 ),
 ( #15345, #17069, #8089 ),
 ( #20371, #1219, #13614 ),
 ( #8213, #22075, #16955 ),
 ( #10047, #1330, #6380 ),
 ( #1093, #22297, #4854 ),
 ( #15244, #6488, #8310 ),
 ( #4734, #11773, #18767 ),
 ( #6588, #3031, #20597 ),
 ( #15123, #4761, #11804 ),
 ( #15269, #22646, #17429 ),
 ( #16989, #10295, #18676 ),
 ( #20394, #15705, #13642 ) ),
 .UNSPECIFIED., .F., .F., .T. ) 
 B_SPLINE_SURFACE_WITH_KNOTS ( ( 4, 2, 2, 2, 2, 2, 4 ),
 ( 3, 3 ),
 ( 6.938893903907228378E-18, 0.001878086432925094810, 0.003756172865850182681, 0.005634259298775270985, 0.007512345731700358423, 0.01126851859755053503, 0.01502469146340070991 ),
 ( 0.000000000000000000, 1.000000000000000000 ),
 .UNSPECIFIED. ) 
 GEOMETRIC_REPRESENTATION_ITEM ( )  RATIONAL_B_SPLINE_SURFACE ( (
 ( 1.000000000000000000, 0.7193398003386572981, 1.000000000000000000),
 ( 1.000000000000000000, 0.7439100388544447329, 1.000000000000000000),
 ( 1.000000000000000000, 0.7665383218960091227, 1.000000000000000000),
 ( 1.000000000000000000, 0.8084046970498726115, 1.000000000000000000),
 ( 1.000000000000000000, 0.8276426232564266794, 1.000000000000000000),
 ( 1.000000000000000000, 0.8630029158315868365, 1.000000000000000000),
 ( 1.000000000000000000, 0.8791524022219731060, 1.000000000000000000),
 ( 1.000000000000000000, 0.9083399791581028282, 1.000000000000000000),
 ( 1.000000000000000000, 0.9212515500168145799, 1.000000000000000000),
 ( 1.000000000000000000, 0.9553996440806984403, 1.000000000000000000),
 ( 1.000000000000000000, 0.9720881558707328285, 1.000000000000000000),
 ( 1.000000000000000000, 0.9943940623865485939, 1.000000000000000000),
 ( 1.000000000000000000, 0.9999834998403251962, 1.000000000000000000),
 ( 1.000000000000000000, 1.000000000000000000, 1.000000000000000000) ) ) 
 REPRESENTATION_ITEM ( '' )  SURFACE ( )  );
#18377=VERTEX_POINT ( 'NONE', #2849 ) ;
#18384=VECTOR ( 'NONE', #3058, 999.9999999999998863 ) ;
#18401=CARTESIAN_POINT ( 'NONE',  ( -14.56978029430814026, 147.5825162344054888, 276.9379655111616785 ) ) ;
#18413=CARTESIAN_POINT ( 'NONE',  ( 3.316624388958365088, 166.4147108432491109, 256.6009726804241495 ) ) ;
#18424=DIRECTION ( 'NONE',  ( 0.009760756503428011724, -0.9999378516499566327, 0.005387065077610982654 ) ) ;
#18441=ORIENTED_EDGE ( 'NONE', *, *, #21003, .F. ) ;
#18482=ORIENTED_EDGE ( 'NONE', *, *, #19705, .T. ) ;
#18489=DIRECTION ( 'NONE',  ( 0.9726991065672924153, 0.2316562896908775926, -0.01384960395994898341 ) ) ;
#18523=CONICAL_SURFACE ( 'NONE', #10446, 14.99999999999997691, 0.03490658503988662564 ) ;
#18525=FACE_OUTER_BOUND ( 'NONE', #4604, .T. ) ;
#18555=CARTESIAN_POINT ( 'NONE',  ( 48.31072223536580879, 166.8507685304811048, 256.0170097695140043 ) ) ;
#18563=CARTESIAN_POINT ( 'NONE',  ( 12.87400438914988321, 189.0062672177662364, 276.1925613188200828 ) ) ;
#18593=EDGE_CURVE ( 'NONE', #2627, #17705, #18884, .T. ) ;
#18619=DIRECTION ( 'NONE',  ( 0.01292394549866738782, 0.005513023399720468239, 0.9999012842304692006 ) ) ;
#18644=CARTESIAN_POINT ( 'NONE',  ( -10.98162931145840027, 147.1570210637436560, 278.5494351491892076 ) ) ;
#18655=EDGE_CURVE ( 'NONE', #17624, #10072, #5197, .T. ) ;
#18662=CARTESIAN_POINT ( 'NONE',  ( 15.56728057410850852, 187.6694373681214927, 276.3106296452654078 ) ) ;
#18676=CARTESIAN_POINT ( 'NONE',  ( -3.143027085112847896, 189.9554771204651900, 275.0835221995262714 ) ) ;
#18678=B_SPLINE_CURVE_WITH_KNOTS ( 'NONE', 3,
 ( #15508, #4569, #11598, #13443, #6749, #2854, #22129, #22236, #6430, #18925, #9865, #16885 ),
 .UNSPECIFIED., .F., .F.,
 ( 4, 2, 2, 2, 2, 4 ),
 ( 0.000000000000000000, 0.003508523874122990941, 0.007017047748245981882, 0.01052557162236897673, 0.01227983355943047111, 0.01403409549649196376 ),
 .UNSPECIFIED. ) ;
#18683=CARTESIAN_POINT ( 'NONE',  ( 9.196690372329099361, 142.8086146031528187, 274.7267082784171066 ) ) ;
#18750=EDGE_LOOP ( 'NONE', ( #12478, #20779, #2497, #8149 ) ) ;
#18755=EDGE_CURVE ( 'NONE', #20552, #20838, #11833, .T. ) ;
#18767=CARTESIAN_POINT ( 'NONE',  ( -8.569456489635145502, 187.5482121046341319, 277.4292011265865767 ) ) ;
#18807=CARTESIAN_POINT ( 'NONE',  ( 13.68126522347680485, 144.1100395844905222, 275.5440367720843824 ) ) ;
#18864=EDGE_LOOP ( 'NONE', ( #7288, #1741 ) ) ;
#18871=CARTESIAN_POINT ( 'NONE',  ( -13.16231198119108114, 149.0364497547966494, 278.8421488773936403 ) ) ;
#18884=LINE ( 'NONE', #13407, #4483 ) ;
#18887=CARTESIAN_POINT ( 'NONE',  ( 19.70989040611666709, 186.5267750472335422, 276.1911881219696738 ) ) ;
#18913=CARTESIAN_POINT ( 'NONE',  ( 19.17420491522518944, 147.8948958764534325, 276.8099206193942905 ) ) ;
#18925=CARTESIAN_POINT ( 'NONE',  ( 10.31485404155361074, 143.0931589593379840, 274.9343155965042342 ) ) ;
#18936=CARTESIAN_POINT ( 'NONE',  ( 48.31072223536580879, 166.8507685304811048, 256.0170097695140043 ) ) ;
#18937=ORIENTED_EDGE ( 'NONE', *, *, #4591, .F. ) ;
#18938=FACE_OUTER_BOUND ( 'NONE', #7456, .T. ) ;
#18944=FACE_OUTER_BOUND ( 'NONE', #12083, .T. ) ;
#18967=VECTOR ( 'NONE', #16023, 1000.000000000000227 ) ;
#18971=ORIENTED_EDGE ( 'NONE', *, *, #9799, .T. ) ;
#18977=CARTESIAN_POINT ( 'NONE',  ( -5.907585137310531032, 144.0910834040820703, 276.2173154596309246 ) ) ;
#18981=CARTESIAN_POINT ( 'NONE',  ( -1.632550740186649252, 142.7036636415817838, 274.8672572718561469 ) ) ;
#18990=ORIENTED_EDGE ( 'NONE', *, *, #5040, .T. ) ;
#18994=DIRECTION ( 'NONE',  ( 0.009760756503427813965, -0.9999378516499565217, 0.005387065077611106687 ) ) ;
#18999=DIRECTION ( 'NONE',  ( 0.009760756503428037745, -0.9999378516499566327, 0.005387065077611006073 ) ) ;
#19007=AXIS2_PLACEMENT_3D ( 'NONE', #7953, #2796, #20237 ) ;
#19009=VECTOR ( 'NONE', #1316, 1000.000000000000000 ) ;
#19015=CARTESIAN_POINT ( 'NONE',  ( 11.38205409781506816, 143.4374251742922866, 275.3786240061384092 ) ) ;
#19029=EDGE_CURVE ( 'NONE', #2627, #15447, #17698, .T. ) ;
#19034=FACE_OUTER_BOUND ( 'NONE', #12017, .T. ) ;
#19086=CARTESIAN_POINT ( 'NONE',  ( -11.34375974262850129, 185.6357169915080760, 278.3389279131694138 ) ) ;
#19090=CARTESIAN_POINT ( 'NONE',  ( -2.775788928915473797, 142.9626891742539669, 275.1092189909475678 ) ) ;
#19108=AXIS2_PLACEMENT_3D ( 'NONE', #5562, #7284, #7181 ) ;
#19118=DIRECTION ( 'NONE',  ( -0.01292394549866738782, -0.005513023399720468239, -0.9999012842304692006 ) ) ;
#19127=FACE_BOUND ( 'NONE', #8143, .T. ) ;
#19128=CARTESIAN_POINT ( 'NONE',  ( 21.10182743699991903, 147.3736716370421789, 276.4577479339097863 ) ) ;
#19138=DIRECTION ( 'NONE',  ( 0.01292394549866738782, 0.005513023399720468239, 0.9999012842304692006 ) ) ;
#19164=DIRECTION ( 'NONE',  ( 0.01292394549866738782, 0.005513023399720468239, 0.9999012842304692006 ) ) ;
#19174=DIRECTION ( 'NONE',  ( 0.01292394549866738782, 0.005513023399720468239, 0.9999012842304692006 ) ) ;
#19184=CARTESIAN_POINT ( 'NONE',  ( 16.46024795975520760, 187.9730162318629425, 275.8249587968540482 ) ) ;
#19186=CIRCLE ( 'NONE', #6367, 24.99999999999998224 ) ;
#19194=EDGE_CURVE ( 'NONE', #6995, #2627, #8531, .T. ) ;
#19204=AXIS2_PLACEMENT_3D ( 'NONE', #22209, #20383, #1112 ) ;
#19210=VECTOR ( 'NONE', #21367, 999.9999999999998863 ) ;
#19235=( BOUNDED_SURFACE ( )  B_SPLINE_SURFACE ( 3, 2, ( 
 ( #16765, #1013, #2842 ),
 ( #16870, #2948, #10304 ),
 ( #19128, #15277, #15716 ),
 ( #20968, #18913, #22225 ),
 ( #17101, #3169, #13978 ),
 ( #22331, #8668, #13650 ),
 ( #1362, #11690, #6843 ),
 ( #17437, #6955, #10420 ),
 ( #1694, #15603, #3407 ),
 ( #16997, #13535, #5107 ),
 ( #18807, #6626, #8338 ),
 ( #6517, #19015, #22659 ),
 ( #15382, #10089, #3277 ),
 ( #18683, #9969, #1260 ) ),
 .UNSPECIFIED., .F., .F., .T. ) 
 B_SPLINE_SURFACE_WITH_KNOTS ( ( 4, 2, 2, 2, 2, 2, 4 ),
 ( 3, 3 ),
 ( 3.903127820947815962E-18, 0.001878086432925129287, 0.003756172865850254672, 0.005634259298775380273, 0.007512345731700505874, 0.01126851859755075708, 0.01502469146340100828 ),
 ( 0.000000000000000000, 1.000000000000000000 ),
 .UNSPECIFIED. ) 
 GEOMETRIC_REPRESENTATION_ITEM ( )  RATIONAL_B_SPLINE_SURFACE ( (
 ( 1.000000000000000000, 0.7193398003386550776, 1.000000000000000000),
 ( 1.000000000000000000, 0.7439100388534258812, 1.000000000000000000),
 ( 1.000000000000000000, 0.7665383218973651491, 1.000000000000000000),
 ( 1.000000000000000000, 0.8084046970485163630, 1.000000000000000000),
 ( 1.000000000000000000, 0.8276426232566694852, 1.000000000000000000),
 ( 1.000000000000000000, 0.8630029158313429205, 1.000000000000000000),
 ( 1.000000000000000000, 0.8791524022210245315, 1.000000000000000000),
 ( 1.000000000000000000, 0.9083399791590486272, 1.000000000000000000),
 ( 1.000000000000000000, 0.9212515500161249093, 1.000000000000000000),
 ( 1.000000000000000000, 0.9553996440820913261, 1.000000000000000000),
 ( 1.000000000000000000, 0.9720881558712876069, 1.000000000000000000),
 ( 1.000000000000000000, 0.9943940623859978123, 1.000000000000000000),
 ( 1.000000000000000000, 0.9999834998407445275, 1.000000000000000000),
 ( 1.000000000000000000, 1.000000000000000000, 1.000000000000000000) ) ) 
 REPRESENTATION_ITEM ( '' )  SURFACE ( )  );
#19271=VERTEX_POINT ( 'NONE', #9637 ) ;
#19282=DIRECTION ( 'NONE',  ( 0.009760756503428003050, -0.9999378516499564107, 0.005387065077611006073 ) ) ;
#19294=ADVANCED_FACE ( 'NONE', ( #1134 ), #19235, .F. ) ;
#19315=CARTESIAN_POINT ( 'NONE',  ( 19.63554660563192300, 184.7628467462468791, 276.5100505641262316 ) ) ;
#19323=CARTESIAN_POINT ( 'NONE',  ( 48.42481440403541626, 171.1166637882075463, 267.9931995069536583 ) ) ;
#19339=FACE_OUTER_BOUND ( 'NONE', #1787, .T. ) ;
#19368=CARTESIAN_POINT ( 'NONE',  ( -2.000285031460988794, 141.9874903446699363, 256.8043760453134610 ) ) ;
#19382=FACE_OUTER_BOUND ( 'NONE', #17377, .T. ) ;
#19435=CARTESIAN_POINT ( 'NONE',  ( 3.600049111542418689, 166.5356125545590373, 278.5290088303507332 ) ) ;
#19452=EDGE_CURVE ( 'NONE', #20449, #15161, #5451, .T. ) ;
#19460=ADVANCED_FACE ( 'NONE', ( #5686 ), #17669, .F. ) ;
#19473=DIRECTION ( 'NONE',  ( 0.01292394549866738782, 0.005513023399720468239, 0.9999012842304692006 ) ) ;
#19485=ORIENTED_EDGE ( 'NONE', *, *, #7864, .T. ) ;
#19493=ADVANCED_FACE ( 'NONE', ( #20039, #4297 ), #13177, .T. ) ;
#19559=VECTOR ( 'NONE', #5342, 1000.000000000000000 ) ;
#19615=CARTESIAN_POINT ( 'NONE',  ( -13.50073983619024176, 183.7065926015648074, 278.6553669534396249 ) ) ;
#19628=CARTESIAN_POINT ( 'NONE',  ( 18.98255855869581410, 147.7934693865291536, 278.2536627479764206 ) ) ;
#19664=FACE_BOUND ( 'NONE', #447, .T. ) ;
#19666=EDGE_CURVE ( 'NONE', #17834, #15668, #21382, .T. ) ;
#19667=EDGE_CURVE ( 'NONE', #6314, #345, #20380, .T. ) ;
#19683=B_SPLINE_CURVE_WITH_KNOTS ( 'NONE', 3,
 ( #9786, #14522, #14867, #2668, #4256, #6214, #16799, #14753, #18075, #18401 ),
 .UNSPECIFIED., .F., .F.,
 ( 4, 2, 2, 2, 4 ),
 ( -3.258122103471980917E-05, 0.003484391791828234802, 0.007001364804691189922, 0.01051833781755414331, 0.01403531083041709843 ),
 .UNSPECIFIED. ) ;
#19691=CARTESIAN_POINT ( 'NONE',  ( -37.32293697913370778, 166.0855081542887319, 269.1292477970816321 ) ) ;
#19705=EDGE_CURVE ( 'NONE', #20838, #7432, #11144, .T. ) ;
#19754=PLANE ( 'NONE',  #12162 ) ;
#19760=CIRCLE ( 'NONE', #15766, 4.200000000000005507 ) ;
#19773=CARTESIAN_POINT ( 'NONE',  ( -9.594263975657968402, 146.1660993649124123, 278.1580113407965769 ) ) ;
#19812=AXIS2_PLACEMENT_3D ( 'NONE', #2495, #21985, #7994 ) ;
#19822=CIRCLE ( 'NONE', #2241, 7.500000000000002665 ) ;
#19829=DIRECTION ( 'NONE',  ( -0.004829518060344538052, -0.03945926991566315462, -0.9992095084480668854 ) ) ;
#19846=AXIS2_PLACEMENT_3D ( 'NONE', #2264, #12839, #9265 ) ;
#19887=EDGE_CURVE ( 'NONE', #3811, #1319, #17024, .T. ) ;
#19976=DIRECTION ( 'NONE',  ( 0.01292394549866738955, 0.005513023399720468239, 0.9999012842304693116 ) ) ;
#19980=CYLINDRICAL_SURFACE ( 'NONE', #20742, 2.000000000000003997 ) ;
#19981=PRODUCT_DEFINITION_SHAPE ( 'NONE', 'NONE',  #7492 ) ;
#20009=ORIENTED_EDGE ( 'NONE', *, *, #16872, .T. ) ;
#20028=CARTESIAN_POINT ( 'NONE',  ( -13.92298191476773894, 185.7071742144165398, 276.7194026170014922 ) ) ;
#20039=FACE_BOUND ( 'NONE', #17264, .T. ) ;
#20040=ORIENTED_EDGE ( 'NONE', *, *, #4507, .F. ) ;
#20044=FACE_OUTER_BOUND ( 'NONE', #12393, .T. ) ;
#20062=DIRECTION ( 'NONE',  ( -0.01292394549866738782, -0.005513023399720468239, -0.9999012842304692006 ) ) ;
#20066=ADVANCED_FACE ( 'NONE', ( #13383 ), #20359, .F. ) ;
#20144=CARTESIAN_POINT ( 'NONE',  ( 11.01344518422641805, 189.7760306036772704, 274.8985146619464786 ) ) ;
#20157=EDGE_CURVE ( 'NONE', #15668, #4798, #14275, .T. ) ;
#20201=DIRECTION ( 'NONE',  ( 0.009760756503427210282, -0.9999378516499566327, 0.005387065077606872227 ) ) ;
#20202=LINE ( 'NONE', #16693, #1541 ) ;
#20216=FACE_OUTER_BOUND ( 'NONE', #16186, .T. ) ;
#20224=CIRCLE ( 'NONE', #14391, 23.67057332475409126 ) ;
#20225=CARTESIAN_POINT ( 'NONE',  ( 51.60019979106838406, 180.9901659820745294, 273.9681169626219344 ) ) ;
#20237=DIRECTION ( 'NONE',  ( 0.009760756503427876415, -0.9999378516499564107, 0.005387065077611007807 ) ) ;
#20244=EDGE_LOOP ( 'NONE', ( #17056, #6835 ) ) ;
#20263=ORIENTED_EDGE ( 'NONE', *, *, #6962, .F. ) ;
#20271=CARTESIAN_POINT ( 'NONE',  ( 8.732865712828660421, 190.3249964942741883, 274.4707185275763095 ) ) ;
#20312=ADVANCED_FACE ( 'NONE', ( #830 ), #9421, .T. ) ;
#20359=CYLINDRICAL_SURFACE ( 'NONE', #10779, 7.999999999999985789 ) ;
#20371=CARTESIAN_POINT ( 'NONE',  ( -12.94603199877754918, 186.2120210550076536, 276.6147472438746604 ) ) ;
#20380=LINE ( 'NONE', #1673, #872 ) ;
#20383=DIRECTION ( 'NONE',  ( 0.01292394549866738782, 0.005513023399720468239, 0.9999012842304692006 ) ) ;
#20384=LINE ( 'NONE', #5924, #1628 ) ;
#20394=CARTESIAN_POINT ( 'NONE',  ( -2.096375399687082197, 190.2200455327031534, 274.6112675210154634 ) ) ;
#20414=CARTESIAN_POINT ( 'NONE',  ( 51.40965114598606078, 154.9164872300239040, 274.0445329540610828 ) ) ;
#20422=EDGE_LOOP ( 'NONE', ( #7349, #16038, #3140, #2953 ) ) ;
#20441=EDGE_CURVE ( 'NONE', #5676, #6995, #10062, .T. ) ;
#20449=VERTEX_POINT ( 'NONE', #3521 ) ;
#20470=CARTESIAN_POINT ( 'NONE',  ( -12.30666638222278308, 148.2435203413120348, 278.7947897727548252 ) ) ;
#20476=CARTESIAN_POINT ( 'NONE',  ( -13.22220441251254286, 184.0858775641920886, 276.8515177789402060 ) ) ;
#20496=VECTOR ( 'NONE', #14767, 1000.000000000000114 ) ;
#20498=EDGE_CURVE ( 'NONE', #8236, #15668, #6448, .T. ) ;
#20503=EDGE_LOOP ( 'NONE', ( #17514, #15692, #13296, #12413 ) ) ;
#20507=CARTESIAN_POINT ( 'NONE',  ( -44.28529243912001334, 178.1224293456637042, 277.1536612075450421 ) ) ;
#20515=DIRECTION ( 'NONE',  ( -0.9726991065672923042, -0.2316562896908775648, 0.01384960395994898168 ) ) ;
#20516=DIRECTION ( 'NONE',  ( 0.01292394549866738782, 0.005513023399720468239, 0.9999012842304692006 ) ) ;
#20528=CARTESIAN_POINT ( 'NONE',  ( -41.44484243847307425, 166.0778875772120671, 275.1831587074827326 ) ) ;
#20538=CARTESIAN_POINT ( 'NONE',  ( 3.833582208905060185, 166.6352317792379267, 296.5970240496429255 ) ) ;
#20552=VERTEX_POINT ( 'NONE', #7196 ) ;
#20559=DIRECTION ( 'NONE',  ( 0.9770372205688159228, -0.2127605332646582692, -0.01145535281434409414 ) ) ;
#20582=CARTESIAN_POINT ( 'NONE',  ( -45.15312007873931321, 180.5703843163154261, 257.1494065962392597 ) ) ;
#20592=EDGE_CURVE ( 'NONE', #5676, #10577, #14573, .T. ) ;
#20593=EDGE_CURVE ( 'NONE', #15824, #17834, #201, .T. ) ;
#20597=CARTESIAN_POINT ( 'NONE',  ( -7.132951983518865724, 188.3585648203603000, 276.8586589376985785 ) ) ;
#20637=ADVANCED_FACE ( 'NONE', ( #14113, #21092 ), #12613, .F. ) ;
#20651=ORIENTED_EDGE ( 'NONE', *, *, #15974, .T. ) ;
#20663=DIRECTION ( 'NONE',  ( 0.01292394549866738782, 0.005513023399720468239, 0.9999012842304692006 ) ) ;
#20674=CARTESIAN_POINT ( 'NONE',  ( -41.71846863476348233, 170.1783921329469251, 257.1623099180083045 ) ) ;
#20683=ORIENTED_EDGE ( 'NONE', *, *, #72, .T. ) ;
#20689=APPLICATION_CONTEXT ( 'automotive_design' ) ;
#20705=AXIS2_PLACEMENT_3D ( 'NONE', #16293, #10547, #22461 ) ;
#20706=CARTESIAN_POINT ( 'NONE',  ( -13.23388004031103193, 148.9771369504019844, 276.9130093688816032 ) ) ;
#20742=AXIS2_PLACEMENT_3D ( 'NONE', #7701, #12547, #3807 ) ;
#20750=ORIENTED_EDGE ( 'NONE', *, *, #2884, .T. ) ;
#20759=EDGE_CURVE ( 'NONE', #5504, #10072, #20384, .T. ) ;
#20760=CARTESIAN_POINT ( 'NONE',  ( 48.31072223536580879, 166.8507685304811048, 256.0170097695140043 ) ) ;
#20762=FACE_OUTER_BOUND ( 'NONE', #20503, .T. ) ;
#20766=ORIENTED_EDGE ( 'NONE', *, *, #9630, .T. ) ;
#20779=ORIENTED_EDGE ( 'NONE', *, *, #20759, .T. ) ;
#20780=( NAMED_UNIT ( * ) SI_UNIT ( $, .STERADIAN. ) SOLID_ANGLE_UNIT ( ) );
#20802=DIRECTION ( 'NONE',  ( -0.01292394549866738608, -0.005513023399720468239, -0.9999012842304692006 ) ) ;
#20808=CARTESIAN_POINT ( 'NONE',  ( -10.43849514614221974, 186.3215578479907037, 278.0845509935722930 ) ) ;
#20812=CARTESIAN_POINT ( 'NONE',  ( -3.901390060011853400, 143.2576375794741068, 275.3477745180629768 ) ) ;
#20837=CARTESIAN_POINT ( 'NONE',  ( 48.49599547156344670, 174.4605628858501802, 275.9746324660413279 ) ) ;
#20838=VERTEX_POINT ( 'NONE', #9615 ) ;
#20853=ADVANCED_FACE ( 'NONE', ( #17420 ), #10080, .T. ) ;
#20857=AXIS2_PLACEMENT_3D ( 'NONE', #7051, #3934, #12357 ) ;
#20863=VERTEX_POINT ( 'NONE', #6724 ) ;
#20898=ORIENTED_EDGE ( 'NONE', *, *, #9098, .T. ) ;
#20904=CARTESIAN_POINT ( 'NONE',  ( 10.97572204090303138, 189.7859119041212637, 274.8914519908082070 ) ) ;
#20952=CARTESIAN_POINT ( 'NONE',  ( 48.53901525512552695, 159.4173909239030706, 268.0562281683617130 ) ) ;
#20966=FACE_OUTER_BOUND ( 'NONE', #17540, .T. ) ;
#20968=CARTESIAN_POINT ( 'NONE',  ( 20.09393204039708181, 146.8369376497900021, 276.4047955799927081 ) ) ;
#20972=AXIS2_PLACEMENT_3D ( 'NONE', #8647, #5083, #12118 ) ;
#20983=ORIENTED_EDGE ( 'NONE', *, *, #8209, .F. ) ;
#21003=EDGE_CURVE ( 'NONE', #10899, #7432, #8957, .T. ) ;
#21008=ORIENTED_EDGE ( 'NONE', *, *, #2, .T. ) ;
#21036=CARTESIAN_POINT ( 'NONE',  ( 3.622049127414185499, 188.3056765838590252, 296.4802766975643635 ) ) ;
#21041=CARTESIAN_POINT ( 'NONE',  ( 14.35565316234159816, 188.7518249220741495, 275.4952485672711191 ) ) ;
#21092=FACE_OUTER_BOUND ( 'NONE', #14019, .T. ) ;
#21110=CARTESIAN_POINT ( 'NONE',  ( -45.15312007873932032, 180.5703843163154261, 257.1494065962392597 ) ) ;
#21118=VECTOR ( 'NONE', #18489, 999.9999999999998863 ) ;
#21124=ORIENTED_EDGE ( 'NONE', *, *, #2884, .F. ) ;
#21140=ADVANCED_FACE ( 'NONE', ( #16727 ), #976, .T. ) ;
#21150=CARTESIAN_POINT ( 'NONE',  ( 18.17462290198324126, 185.9111733914936053, 277.9589104919019746 ) ) ;
#21177=SHAPE_REPRESENTATION ( 'Flange', ( #6292 ), #21305 ) ;
#21188=ORIENTED_EDGE ( 'NONE', *, *, #7129, .T. ) ;
#21199=DIRECTION ( 'NONE',  ( -0.009760756503428009989, 0.9999378516499564107, -0.005387065077611111891 ) ) ;
#21222=MECHANICAL_DESIGN_GEOMETRIC_PRESENTATION_REPRESENTATION('',(#10238),#14290);
#21234=CARTESIAN_POINT ( 'NONE',  ( 11.27670803124779297, 143.4306312998254214, 275.5969523110588284 ) ) ;
#21239=CARTESIAN_POINT ( 'NONE',  ( 51.87369047120967025, 152.9724930639170282, 274.1190593707768812 ) ) ;
#21243=ORIENTED_EDGE ( 'NONE', *, *, #5219, .F. ) ;
#21269=ORIENTED_EDGE ( 'NONE', *, *, #19887, .F. ) ;
#21272=EDGE_CURVE ( 'NONE', #5251, #6123, #22027, .T. ) ;
#21274=ORIENTED_EDGE ( 'NONE', *, *, #584, .F. ) ;
#21277=CIRCLE ( 'NONE', #19812, 2.000000000000006217 ) ;
#21305=( GEOMETRIC_REPRESENTATION_CONTEXT ( 3 ) GLOBAL_UNCERTAINTY_ASSIGNED_CONTEXT ( ( #40 ) ) GLOBAL_UNIT_ASSIGNED_CONTEXT ( ( #13566, #3201, #20780 ) ) REPRESENTATION_CONTEXT ( 'NONE', 'WORKASPACE' ) );
#21332=ADVANCED_FACE ( 'NONE', ( #489, #7491 ), #19754, .T. ) ;
#21337=DIRECTION ( 'NONE',  ( 0.01292394549866738782, 0.005513023399720468239, 0.9999012842304692006 ) ) ;
#21357=ADVANCED_FACE ( 'NONE', ( #20216 ), #4362, .F. ) ;
#21367=DIRECTION ( 'NONE',  ( 0.9770372205688160339, -0.2127605332646582970, -0.01145535281434409587 ) ) ;
#21382=CIRCLE ( 'NONE', #15545, 15.00000000000000533 ) ;
#21393=CARTESIAN_POINT ( 'NONE',  ( -1.761514441332976855, 142.7342175572188694, 274.9248293644216687 ) ) ;
#21414=ORIENTED_EDGE ( 'NONE', *, *, #3629, .F. ) ;
#21425=CARTESIAN_POINT ( 'NONE',  ( -44.28529243912000624, 178.1224293456637042, 277.1536612075450421 ) ) ;
#21431=DIRECTION ( 'NONE',  ( -0.9770372205688159228, 0.2127605332646583802, 0.01145535281434409414 ) ) ;
#21457=CARTESIAN_POINT ( 'NONE',  ( -4.656860399053663890, 189.4255402448441714, 275.7688761517259763 ) ) ;
#21466=ORIENTED_EDGE ( 'NONE', *, *, #18655, .T. ) ;
#21471=CIRCLE ( 'NONE', #10114, 8.000000000000012434 ) ;
#21481=FACE_OUTER_BOUND ( 'NONE', #16419, .T. ) ;
#21492=ORIENTED_EDGE ( 'NONE', *, *, #6692, .F. ) ;
#21500=CARTESIAN_POINT ( 'NONE',  ( -12.30122876842438373, 148.2386865495960251, 278.7941984645188427 ) ) ;
#21504=CARTESIAN_POINT ( 'NONE',  ( 18.61477174969464699, 185.5695927475049132, 278.0502835483144395 ) ) ;
#21506=CARTESIAN_POINT ( 'NONE',  ( 3.596201236416850744, 188.2946505370595673, 294.4804741291034134 ) ) ;
#21507=DIRECTION ( 'NONE',  ( -0.7056475024472774749, 0.7085438702141408918, 0.005214045635221195574 ) ) ;
#21523=CARTESIAN_POINT ( 'NONE',  ( 3.575103298931712636, 166.5249713112435188, 276.5989983650335375 ) ) ;
#21551=ORIENTED_EDGE ( 'NONE', *, *, #8103, .F. ) ;
#21555=EDGE_LOOP ( 'NONE', ( #5345, #10466, #15376, #20898, #3691, #20009, #7411, #10048, #6255, #14070 ) ) ;
#21575=CARTESIAN_POINT ( 'NONE',  ( -41.44394036008644377, 166.0782723806960064, 275.2529508106263734 ) ) ;
#21582=DIRECTION ( 'NONE',  ( 0.01292394549866738782, 0.005513023399720468239, 0.9999012842304692006 ) ) ;
#21610=CARTESIAN_POINT ( 'NONE',  ( 9.196690372329049623, 142.8086146031528187, 274.7267082784170498 ) ) ;
#21695=EDGE_CURVE ( 'NONE', #8236, #15824, #13660, .T. ) ;
#21696=DIRECTION ( 'NONE',  ( 0.2129978593076544968, 0.9766860055760742121, 0.02676487328961881657 ) ) ;
#21713=EDGE_CURVE ( 'NONE', #6385, #3811, #20202, .T. ) ;
#21726=CARTESIAN_POINT ( 'NONE',  ( -9.732840034447848510, 187.7216402471333083, 276.1639041411631865 ) ) ;
#21730=CARTESIAN_POINT ( 'NONE',  ( 15.82374578500689211, 187.4932621794992258, 277.2901064574259067 ) ) ;
#21777=AXIS2_PLACEMENT_3D ( 'NONE', #21506, #3845, #10618 ) ;
#21844=DIRECTION ( 'NONE',  ( 0.01292394549866738782, 0.005513023399720468239, 0.9999012842304692006 ) ) ;
#21862=DIRECTION ( 'NONE',  ( 0.01292394549866738782, 0.005513023399720468239, 0.9999012842304692006 ) ) ;
#21873=ORIENTED_EDGE ( 'NONE', *, *, #2338, .F. ) ;
#21937=CARTESIAN_POINT ( 'NONE',  ( -6.504117289611111019, 188.9465505160917473, 275.5474451934275635 ) ) ;
#21945=CARTESIAN_POINT ( 'NONE',  ( 9.391523084377633168, 190.1646184555798129, 274.7467018831596306 ) ) ;
#21947=DIRECTION ( 'NONE',  ( 0.2320196626118057881, -0.9719970830534312434, 0.03726320835790866703 ) ) ;
#21985=DIRECTION ( 'NONE',  ( -0.7084451806051488276, -0.7056452299526765337, 0.01304743355500853977 ) ) ;
#22009=FACE_OUTER_BOUND ( 'NONE', #5294, .T. ) ;
#22027=CIRCLE ( 'NONE', #22386, 7.500000000000002665 ) ;
#22040=ORIENTED_EDGE ( 'NONE', *, *, #6962, .T. ) ;
#22049=ORIENTED_EDGE ( 'NONE', *, *, #14121, .F. ) ;
#22068=CARTESIAN_POINT ( 'NONE',  ( -1.632550740186646365, 142.7036636415817838, 274.8672572718561469 ) ) ;
#22075=CARTESIAN_POINT ( 'NONE',  ( -11.58738668730085841, 185.5101712897686355, 277.0082871630683030 ) ) ;
#22129=CARTESIAN_POINT ( 'NONE',  ( 13.62697418300035679, 144.0917254245173353, 275.5345564924090809 ) ) ;
#22142=CIRCLE ( 'NONE', #15968, 14.99999999999997691 ) ;
#22155=DIRECTION ( 'NONE',  ( -0.005493774068846061544, 0.02859024303483492097, -0.9995761183870338629 ) ) ;
#22168=PLANE ( 'NONE',  #18055 ) ;
#22172=( BOUNDED_SURFACE ( )  B_SPLINE_SURFACE ( 3, 2, ( 
 ( #20271, #994, #9611 ),
 ( #890, #7881, #14920 ),
 ( #20144, #7980, #15019 ),
 ( #13298, #4534, #18563 ),
 ( #21041, #15254, #15902 ),
 ( #4745, #18662, #3044 ),
 ( #11789, #4642, #6718 ),
 ( #2927, #11669, #6500 ),
 ( #10165, #22207, #5397 ),
 ( #2821, #4865, #21150 ),
 ( #18887, #13512, #10066 ),
 ( #1340, #19315, #1448 ),
 ( #8106, #14057, #13411 ),
 ( #9829, #3575, #145 ) ),
 .UNSPECIFIED., .F., .F., .T. ) 
 B_SPLINE_SURFACE_WITH_KNOTS ( ( 4, 2, 2, 2, 2, 2, 4 ),
 ( 3, 3 ),
 ( -0.01502904264599901930, -0.01127178198449926318, -0.007514521322999507917, -0.005635890992249629854, -0.003757260661499752224, -0.001878630330749874377, 3.469446951953614189E-18 ),
 ( 0.000000000000000000, 1.000000000000000000 ),
 .UNSPECIFIED. ) 
 GEOMETRIC_REPRESENTATION_ITEM ( )  RATIONAL_B_SPLINE_SURFACE ( (
 ( 1.000000000000000000, 1.000000000000000000, 1.000000000000000000),
 ( 1.000000000000000000, 0.9999832193767735911, 1.000000000000000000),
 ( 1.000000000000000000, 0.9943958665397538699, 1.000000000000000000),
 ( 1.000000000000000000, 0.9719875995037652316, 1.000000000000000000),
 ( 1.000000000000000000, 0.9551974090686941032, 1.000000000000000000),
 ( 1.000000000000000000, 0.9207014414826584225, 1.000000000000000000),
 ( 1.000000000000000000, 0.9076211955285893307, 1.000000000000000000),
 ( 1.000000000000000000, 0.8785736512487225536, 1.000000000000000000),
 ( 1.000000000000000000, 0.8625652577268398957, 1.000000000000000000),
 ( 1.000000000000000000, 0.8274118182194920568, 1.000000000000000000),
 ( 1.000000000000000000, 0.8082693262200102424, 1.000000000000000000),
 ( 1.000000000000000000, 0.7665332262304687116, 1.000000000000000000),
 ( 1.000000000000000000, 0.7439399906336684465, 1.000000000000000000),
 ( 1.000000000000000000, 0.7193398003386514139, 1.000000000000000000) ) ) 
 REPRESENTATION_ITEM ( '' )  SURFACE ( )  );
#22203=AXIS2_PLACEMENT_3D ( 'NONE', #1827, #6991, #19282 ) ;
#22207=CARTESIAN_POINT ( 'NONE',  ( 17.48198728475768249, 186.4531915267186264, 276.5831127856608305 ) ) ;
#22209=CARTESIAN_POINT ( 'NONE',  ( 3.833582208905060185, 166.6352317792379267, 296.5970240496429255 ) ) ;
#22225=CARTESIAN_POINT ( 'NONE',  ( 18.98968904741751729, 147.7994345178613287, 278.2549083691532701 ) ) ;
#22236=CARTESIAN_POINT ( 'NONE',  ( 11.97803979754709403, 143.5698177053941436, 275.2396454285085383 ) ) ;
#22240=DIRECTION ( 'NONE',  ( 0.9726991065672934145, 0.2316562896908731239, -0.01384960395994897300 ) ) ;
#22254=LINE ( 'NONE', #6657, #7103 ) ;
#22288=CARTESIAN_POINT ( 'NONE',  ( 9.785202419441143107, 190.0604574230576702, 274.9118766335186024 ) ) ;
#22292=CARTESIAN_POINT ( 'NONE',  ( -11.65206543345498602, 147.5984083283656787, 277.2097828948077449 ) ) ;
#22297=CARTESIAN_POINT ( 'NONE',  ( -10.23725882687554112, 186.5193182284470197, 276.8889396700154748 ) ) ;
#22321=LINE ( 'NONE', #20837, #18384 ) ;
#22331=CARTESIAN_POINT ( 'NONE',  ( 18.54079482392480926, 146.0746420647028003, 276.2612673939528918 ) ) ;
#22342=CONICAL_SURFACE ( 'NONE', #6950, 24.99999999999998224, 0.03490658503988662564 ) ;
#22348=CARTESIAN_POINT ( 'NONE',  ( -41.67747345744908216, 165.9786531560170886, 257.1849355913342379 ) ) ;
#22386=AXIS2_PLACEMENT_3D ( 'NONE', #10152, #1428, #3232 ) ;
#22388=ORIENTED_EDGE ( 'NONE', *, *, #20441, .T. ) ;
#22391=CIRCLE ( 'NONE', #15835, 24.99999999999998224 ) ;
#22415=ORIENTED_EDGE ( 'NONE', *, *, #19705, .F. ) ;
#22421=AXIS2_PLACEMENT_3D ( 'NONE', #5116, #19138, #3416 ) ;
#22451=EDGE_CURVE ( 'NONE', #16920, #15659, #7148, .T. ) ;
#22461=DIRECTION ( 'NONE',  ( 0.2126763768167733992, 0.9770888199431678744, -0.008136134595576589509 ) ) ;
#22464=DIRECTION ( 'NONE',  ( 0.009760756503427210282, -0.9999378516499566327, 0.005387065077606872227 ) ) ;
#22488=CARTESIAN_POINT ( 'NONE',  ( -13.50073983619024531, 183.7065926015648074, 278.6553669534395681 ) ) ;
#22491=VECTOR ( 'NONE', #21431, 1000.000000000000114 ) ;
#22496=ORIENTED_EDGE ( 'NONE', *, *, #14121, .T. ) ;
#22507=CARTESIAN_POINT ( 'NONE',  ( -2.096375399687102625, 190.2200455327031818, 274.6112675210154634 ) ) ;
#22512=CIRCLE ( 'NONE', #11554, 2.000000000000006661 ) ;
#22513=ADVANCED_FACE ( 'NONE', ( #21481 ), #16575, .F. ) ;
#22514=CARTESIAN_POINT ( 'NONE',  ( -12.73793622217206156, 148.6298842822529878, 278.8389053497636496 ) ) ;
#22575=ORIENTED_EDGE ( 'NONE', *, *, #10206, .T. ) ;
#22594=CARTESIAN_POINT ( 'NONE',  ( 3.394697517040290435, 158.4152025170260742, 256.6430692997608389 ) ) ;
#22620=DIRECTION ( 'NONE',  ( 0.01292394549866738782, 0.005513023399720468239, 0.9999012842304692006 ) ) ;
#22646=CARTESIAN_POINT ( 'NONE',  ( -4.264070500929974195, 189.5987719431177538, 275.3263399216110088 ) ) ;
#22659=CARTESIAN_POINT ( 'NONE',  ( 11.28650372074689834, 143.4152113759959377, 275.6042146768694465 ) ) ;
ENDSEC;
END-ISO-10303-21;
